ISO-10303-21;
HEADER;
FILE_DESCRIPTION (('STEP AP214'),
    '1' );
FILE_NAME ('Parallelogram front_FRONT.step',
    '2026-10-12T23:53:07',
    ( '' ),
    ( '' ),
    'SwSTEP 2.0',
    'SolidWorks 2024',
    '' );
FILE_SCHEMA (( 'AUTOMOTIVE_DESIGN' ));
ENDSEC;

DATA;
#18=ORIENTED_EDGE ( 'NONE', *, *, #35646, .F. ) ;
#42=CARTESIAN_POINT ( 'NONE',  ( -0.1105199412301896417, -0.5049077968913929793, 0.1209919789212513253 ) ) ;
#50=FACE_OUTER_BOUND ( 'NONE', #29896, .T. ) ;
#51=VERTEX_POINT ( 'NONE', #15776 ) ;
#69=FACE_OUTER_BOUND ( 'NONE', #19030, .T. ) ;
#170=B_SPLINE_CURVE_WITH_KNOTS ( 'NONE', 3,
 ( #2399, #24613, #27897, #39613, #37341, #14514 ),
 .UNSPECIFIED., .F., .F.,
 ( 4, 2, 4 ),
 ( 0.0002303018524726754336, 0.0008163183685728737319, 0.001402334884673072084 ),
 .UNSPECIFIED. ) ;
#183=CIRCLE ( 'NONE', #23151, 2.001674066779347783 ) ;
#188=DIRECTION ( 'NONE',  ( -0.05576617208936890391, -0.2535907321052876529, -0.9657027879429589401 ) ) ;
#221=CARTESIAN_POINT ( 'NONE',  ( -0.1212602504878774051, -0.5073146173917495450, 0.1497995784944541608 ) ) ;
#238=CYLINDRICAL_SURFACE ( 'NONE', #20468, 0.06000000000000031697 ) ;
#249=CARTESIAN_POINT ( 'NONE',  ( -0.1045574869087414066, -0.4741643323009803734, 0.09813923389047436718 ) ) ;
#264=ORIENTED_EDGE ( 'NONE', *, *, #34115, .T. ) ;
#271=AXIS2_PLACEMENT_3D ( 'NONE', #761, #13482, #6887 ) ;
#285=CARTESIAN_POINT ( 'NONE',  ( -0.1743922129835730472, -0.5166151207188712791, 0.08499999999999964528 ) ) ;
#297=EDGE_CURVE ( 'NONE', #16265, #14568, #3667, .T. ) ;
#331=DIRECTION ( 'NONE',  ( -7.771561172376107616E-16, 7.170354002788761615E-17, -1.000000000000000000 ) ) ;
#364=DIRECTION ( 'NONE',  ( 0.8150167559926670968, 0.5794373887239150367, 0.000000000000000000 ) ) ;
#367=ORIENTED_EDGE ( 'NONE', *, *, #29637, .T. ) ;
#373=B_SPLINE_CURVE_WITH_KNOTS ( 'NONE', 3,
 ( #29818, #10683, #13963, #23257 ),
 .UNSPECIFIED., .F., .F.,
 ( 4, 4 ),
 ( 8.673617379883828435E-19, 0.0003934542678113513874 ),
 .UNSPECIFIED. ) ;
#375=TOROIDAL_SURFACE ( 'NONE', #39044, 0.04500000000000032446, 0.01499999999999999944 ) ;
#436=CARTESIAN_POINT ( 'NONE',  ( -0.1211772861969157844, -0.5069185045468641571, 0.1468025672055966735 ) ) ;
#458=ORIENTED_EDGE ( 'NONE', *, *, #30646, .F. ) ;
#476=CARTESIAN_POINT ( 'NONE',  ( -0.1127677449505191248, -0.5183788106019665554, 0.3108513529153781318 ) ) ;
#498=SHAPE_DEFINITION_REPRESENTATION ( #951, #40103 ) ;
#509=DIRECTION ( 'NONE',  ( -7.771561172376107616E-16, 7.170354002788761615E-17, -1.000000000000000000 ) ) ;
#570=CARTESIAN_POINT ( 'NONE',  ( -0.2666757540196703080, 0.4921670437878978843, 0.3599999999999995981 ) ) ;
#605=ORIENTED_EDGE ( 'NONE', *, *, #38870, .F. ) ;
#621=FACE_OUTER_BOUND ( 'NONE', #9902, .T. ) ;
#628=EDGE_CURVE ( 'NONE', #28266, #4670, #1089, .T. ) ;
#640=CARTESIAN_POINT ( 'NONE',  ( -0.2300000000000000100, 0.5182417262804744906, 0.3749999999999995559 ) ) ;
#680=CARTESIAN_POINT ( 'NONE',  ( -0.2789010053595594729, 0.4834754829570393486, 0.3749999999999995559 ) ) ;
#702=CARTESIAN_POINT ( 'NONE',  ( -0.1710642718812835639, 0.4986889572247753533, 0.1481991563822706581 ) ) ;
#729=ORIENTED_EDGE ( 'NONE', *, *, #20999, .T. ) ;
#739=FACE_OUTER_BOUND ( 'NONE', #35381, .T. ) ;
#757=DIRECTION ( 'NONE',  ( -1.000000000000000000, 1.421355798447627143E-14, -7.801168736956215639E-16 ) ) ;
#761=CARTESIAN_POINT ( 'NONE',  ( -0.1969433606228600808, 0.5138636982738217229, 0.1528658435937000626 ) ) ;
#857=ORIENTED_EDGE ( 'NONE', *, *, #27787, .T. ) ;
#864=AXIS2_PLACEMENT_3D ( 'NONE', #285, #6192, #12993 ) ;
#869=CARTESIAN_POINT ( 'NONE',  ( -0.1683849832494448140, 0.4901165368553581092, 0.3263506530378934012 ) ) ;
#925=( CONVERSION_BASED_UNIT ( 'INCH', #9929 ) LENGTH_UNIT ( ) NAMED_UNIT ( #28861 ) );
#951=PRODUCT_DEFINITION_SHAPE ( 'NONE', 'NONE',  #8373 ) ;
#994=LINE ( 'NONE', #10008, #35547 ) ;
#1011=CARTESIAN_POINT ( 'NONE',  ( -0.1167294259372888832, -0.5331983348239501819, 0.3749999999999990008 ) ) ;
#1036=DIRECTION ( 'NONE',  ( -7.771561172376107616E-16, 7.170354002788761615E-17, -1.000000000000000000 ) ) ;
#1040=CARTESIAN_POINT ( 'NONE',  ( -0.1743922129835729085, -0.5166151207188712791, 0.3599999999999990430 ) ) ;
#1045=DIRECTION ( 'NONE',  ( 1.000000000000000000, 1.864905829289486282E-14, 8.132394101956133308E-16 ) ) ;
#1089=CIRCLE ( 'NONE', #18239, 0.03000000000000022787 ) ;
#1099=CIRCLE ( 'NONE', #7599, 2.001674066779347783 ) ;
#1112=ORIENTED_EDGE ( 'NONE', *, *, #28978, .F. ) ;
#1126=( CONVERSION_BASED_UNIT ( 'INCH', #10967 ) LENGTH_UNIT ( ) NAMED_UNIT ( #23398 ) );
#1160=CARTESIAN_POINT ( 'NONE',  ( -0.1044436713285742807, -0.4741860147766008837, 0.3606502365330823690 ) ) ;
#1183=ORIENTED_EDGE ( 'NONE', *, *, #19480, .T. ) ;
#1186=CARTESIAN_POINT ( 'NONE',  ( -1.019575837292303166, -0.04310840302197994911, 0.3749999999999990008 ) ) ;
#1198=CARTESIAN_POINT ( 'NONE',  ( -0.1531325081225953788, 0.4743613400439437022, 0.3600421117866457466 ) ) ;
#1267=CARTESIAN_POINT ( 'NONE',  ( -0.1529745177444690185, 0.4738847129974373962, 0.3606502365071603822 ) ) ;
#1275=DIRECTION ( 'NONE',  ( -1.000000000000000000, 0.000000000000000000, -5.691349986800505477E-16 ) ) ;
#1276=CARTESIAN_POINT ( 'NONE',  ( -0.1743922129835729085, -0.5166151207188712791, 0.3750000000000001110 ) ) ;
#1321=EDGE_CURVE ( 'NONE', #10838, #32882, #34705, .T. ) ;
#1360=ADVANCED_FACE ( 'NONE', ( #3388 ), #19225, .T. ) ;
#1372=EDGE_CURVE ( 'NONE', #16786, #1527, #17823, .T. ) ;
#1410=CARTESIAN_POINT ( 'NONE',  ( -1.019575837292303166, -0.04310840302197994911, 0.3749999999999990008 ) ) ;
#1422=CIRCLE ( 'NONE', #6633, 2.001674066779347783 ) ;
#1435=CARTESIAN_POINT ( 'NONE',  ( -0.1617555154933660866, 0.4683069300263329460, 0.1178658435716244679 ) ) ;
#1455=CARTESIAN_POINT ( 'NONE',  ( -0.1553124468364784072, 0.4816356660588179128, 0.3589899338161260944 ) ) ;
#1459=( BOUNDED_SURFACE ( )  B_SPLINE_SURFACE ( 3, 2, ( 
 ( #10089, #35198, #16668 ),
 ( #6999, #4506, #1267 ),
 ( #32284, #7600, #19567 ),
 ( #3907, #23263, #16462 ),
 ( #29005, #35581, #20173 ),
 ( #869, #4103, #10308 ),
 ( #29220, #13376, #22874 ),
 ( #35389, #38670, #13771 ),
 ( #7381, #19957, #26334 ),
 ( #33710, #30639, #30213 ),
 ( #23476, #5521, #17271 ),
 ( #39082, #21173, #17866 ) ),
 .UNSPECIFIED., .F., .F., .F. ) 
 B_SPLINE_SURFACE_WITH_KNOTS ( ( 4, 2, 2, 2, 2, 4 ),
 ( 3, 3 ),
 ( 0.001713391272003884783, 0.002288612648294801721, 0.002863834024585718441, 0.003151444712731176802, 0.003439055400876635596, 0.004014276777167552317 ),
 ( 0.000000000000000000, 1.000000000000000000 ),
 .UNSPECIFIED. ) 
 GEOMETRIC_REPRESENTATION_ITEM ( )  RATIONAL_B_SPLINE_SURFACE ( (
 ( 1.000000000000000000, 0.9128709291752516997, 1.000000000000000000),
 ( 1.000000000000000000, 0.9128719127420300561, 1.000000000000000000),
 ( 1.000000000000000000, 0.9128123349199704917, 1.000000000000000000),
 ( 1.000000000000000000, 0.9126095266099195635, 1.000000000000000000),
 ( 1.000000000000000000, 0.9124632789542336253, 1.000000000000000000),
 ( 1.000000000000000000, 0.9122369551432389922, 1.000000000000000000),
 ( 1.000000000000000000, 0.9121592698944432920, 1.000000000000000000),
 ( 1.000000000000000000, 0.9120159902104399974, 1.000000000000000000),
 ( 1.000000000000000000, 0.9119497308967260407, 1.000000000000000000),
 ( 1.000000000000000000, 0.9117802546610581649, 1.000000000000000000),
 ( 1.000000000000000000, 0.9117114107492867436, 1.000000000000000000),
 ( 1.000000000000000000, 0.9117127123830562896, 1.000000000000000000) ) ) 
 REPRESENTATION_ITEM ( '' )  SURFACE ( )  );
#1469=DIRECTION ( 'NONE',  ( -1.000000000000000000, 0.000000000000000000, -1.138269997360105631E-15 ) ) ;
#1527=VERTEX_POINT ( 'NONE', #11997 ) ;
#1560=CARTESIAN_POINT ( 'NONE',  ( -0.2267371898560517907, -0.4872893062166330780, 0.3599999999999990430 ) ) ;
#1580=VECTOR ( 'NONE', #3908, 39.37007874015748143 ) ;
#1585=DIRECTION ( 'NONE',  ( -7.771561172376107616E-16, 7.170354002788761615E-17, -1.000000000000000000 ) ) ;
#1601=ORIENTED_EDGE ( 'NONE', *, *, #39876, .T. ) ;
#1627=DIRECTION ( 'NONE',  ( -7.771561172376107616E-16, 7.170354002788761615E-17, -1.000000000000000000 ) ) ;
#1644=CIRCLE ( 'NONE', #37731, 0.04500000000000022038 ) ;
#1683=ORIENTED_EDGE ( 'NONE', *, *, #13917, .F. ) ;
#1732=ADVANCED_FACE ( 'NONE', ( #23607 ), #35570, .T. ) ;
#1752=VERTEX_POINT ( 'NONE', #23419 ) ;
#1757=ORIENTED_EDGE ( 'NONE', *, *, #5929, .T. ) ;
#1772=AXIS2_PLACEMENT_3D ( 'NONE', #6632, #19208, #37715 ) ;
#1779=DIRECTION ( 'NONE',  ( 1.000000000000000000, 0.000000000000000000, 7.702990362679453920E-16 ) ) ;
#1837=DIRECTION ( 'NONE',  ( 7.771561172376107616E-16, -7.170354002788761615E-17, 1.000000000000000000 ) ) ;
#1859=DIRECTION ( 'NONE',  ( -1.000000000000000000, 0.000000000000000000, 0.000000000000000000 ) ) ;
#1902=EDGE_CURVE ( 'NONE', #26889, #39656, #5328, .T. ) ;
#1909=CARTESIAN_POINT ( 'NONE',  ( -0.1795773455677913688, 0.4580325878418424757, 0.3606502365332823201 ) ) ;
#1936=EDGE_LOOP ( 'NONE', ( #36678, #33675, #17468, #17857 ) ) ;
#1971=EDGE_CURVE ( 'NONE', #17060, #35941, #170, .T. ) ;
#1984=DIRECTION ( 'NONE',  ( 7.771561172376107616E-16, -7.170354002788761615E-17, 1.000000000000000000 ) ) ;
#2026=CARTESIAN_POINT ( 'NONE',  ( -0.1631308187679525179, 0.4729065765976191993, 0.1187908002253880019 ) ) ;
#2030=EDGE_LOOP ( 'NONE', ( #22026, #38650, #7429 ) ) ;
#2105=AXIS2_PLACEMENT_3D ( 'NONE', #10033, #22605, #6526 ) ;
#2108=CIRCLE ( 'NONE', #29680, 2.001671648589471442 ) ;
#2120=ORIENTED_EDGE ( 'NONE', *, *, #23131, .T. ) ;
#2142=B_SPLINE_CURVE_WITH_KNOTS ( 'NONE', 3,
 ( #25681, #221, #436, #16227 ),
 .UNSPECIFIED., .F., .F.,
 ( 4, 4 ),
 ( 4.336808689942155440E-19, 0.0002303018524726754336 ),
 .UNSPECIFIED. ) ;
#2183=CARTESIAN_POINT ( 'NONE',  ( -0.2299999999999999267, 0.5182417262804744906, 0.09999999999999989453 ) ) ;
#2191=TOROIDAL_SURFACE ( 'NONE', #4167, 0.04500000000000023426, 0.01499999999999999944 ) ;
#2207=DIRECTION ( 'NONE',  ( -7.771561172376107616E-16, 7.170354002788761615E-17, -1.000000000000000000 ) ) ;
#2228=EDGE_CURVE ( 'NONE', #36405, #9596, #6331, .T. ) ;
#2232=CARTESIAN_POINT ( 'NONE',  ( -2.070754768975505034, -0.09959325338431362917, 0.3602693341844379060 ) ) ;
#2270=AXIS2_PLACEMENT_3D ( 'NONE', #4986, #30096, #17553 ) ;
#2276=AXIS2_PLACEMENT_3D ( 'NONE', #17712, #30687, #30076 ) ;
#2279=AXIS2_PLACEMENT_3D ( 'NONE', #37055, #15466, #2914 ) ;
#2280=CARTESIAN_POINT ( 'NONE',  ( -0.1068489084554249124, -0.4866459697499495585, 0.09652185631082288442 ) ) ;
#2295=CARTESIAN_POINT ( 'NONE',  ( -0.1710642718812830643, 0.4986889572247755198, 0.3032895567580806695 ) ) ;
#2297=EDGE_LOOP ( 'NONE', ( #19537, #21661, #39362, #36100 ) ) ;
#2326=ORIENTED_EDGE ( 'NONE', *, *, #26541, .T. ) ;
#2399=CARTESIAN_POINT ( 'NONE',  ( -0.1210148435730033917, -0.5061394519556894345, 0.1438724812234795092 ) ) ;
#2409=FACE_BOUND ( 'NONE', #23150, .T. ) ;
#2462=EDGE_CURVE ( 'NONE', #1752, #51, #373, .T. ) ;
#2478=ORIENTED_EDGE ( 'NONE', *, *, #19314, .T. ) ;
#2479=CARTESIAN_POINT ( 'NONE',  ( -0.1157923916714846541, -0.5295015842442638565, 0.1380392329925947958 ) ) ;
#2502=CARTESIAN_POINT ( 'NONE',  ( -0.1743922129835729085, -0.5166151207188712791, 0.3750000000000001110 ) ) ;
#2598=DIRECTION ( 'NONE',  ( 1.000000000000000000, -3.406373435249580326E-19, 7.771561172376097755E-16 ) ) ;
#2629=CARTESIAN_POINT ( 'NONE',  ( -0.1642263572652579717, 0.5103503757440955857, 0.1470331037154087028 ) ) ;
#2634=FACE_BOUND ( 'NONE', #15881, .T. ) ;
#2656=CARTESIAN_POINT ( 'NONE',  ( -0.2600000000000002309, 0.5182417262804744906, 0.3749999999999995559 ) ) ;
#2672=CARTESIAN_POINT ( 'NONE',  ( -0.1190772264498593247, -0.4967457283353788888, 0.1275078045371980107 ) ) ;
#2736=B_SPLINE_CURVE_WITH_KNOTS ( 'NONE', 3,
 ( #2295, #8443, #37036, #33746, #36219, #17700, #4951, #5558, #33338, #23693 ),
 .UNSPECIFIED., .F., .F.,
 ( 4, 2, 2, 2, 4 ),
 ( 0.001421410091499676447, 0.001776295181873929763, 0.002131180272248183079, 0.002486065362622435961, 0.002840950452996689277 ),
 .UNSPECIFIED. ) ;
#2753=ADVANCED_FACE ( 'NONE', ( #15560 ), #13441, .T. ) ;
#2791=CARTESIAN_POINT ( 'NONE',  ( -0.1167294259372886195, -0.5331983348239496268, 0.1476740372344541030 ) ) ;
#2805=CARTESIAN_POINT ( 'NONE',  ( -0.2299999999999999267, 0.5182417262804744906, 0.09999999999999989453 ) ) ;
#2830=ORIENTED_EDGE ( 'NONE', *, *, #10049, .F. ) ;
#2860=LINE ( 'NONE', #2656, #25294 ) ;
#2869=CIRCLE ( 'NONE', #35041, 0.03000000000000002318 ) ;
#2872=ORIENTED_EDGE ( 'NONE', *, *, #18200, .T. ) ;
#2882=ORIENTED_EDGE ( 'NONE', *, *, #14497, .T. ) ;
#2914=DIRECTION ( 'NONE',  ( 1.000000000000000000, 1.243043370174342012E-14, 7.886895865933756492E-16 ) ) ;
#2946=EDGE_CURVE ( 'NONE', #17948, #9996, #8549, .T. ) ;
#2950=FACE_OUTER_BOUND ( 'NONE', #8425, .T. ) ;
#2961=DIRECTION ( 'NONE',  ( 0.000000000000000000, 0.000000000000000000, 1.000000000000000000 ) ) ;
#2980=ORIENTED_EDGE ( 'NONE', *, *, #12448, .F. ) ;
#2984=ORIENTED_EDGE ( 'NONE', *, *, #11756, .T. ) ;
#3035=DIRECTION ( 'NONE',  ( -7.771561172376107616E-16, 7.170354002788761615E-17, -1.000000000000000000 ) ) ;
#3064=EDGE_LOOP ( 'NONE', ( #6546, #9568 ) ) ;
#3087=FACE_OUTER_BOUND ( 'NONE', #18565, .T. ) ;
#3109=CARTESIAN_POINT ( 'NONE',  ( -0.2299999999999999267, 0.5182417262804744906, 0.3599999999999993205 ) ) ;
#3345=CARTESIAN_POINT ( 'NONE',  ( -0.1969433606228599420, 0.5138636982738220560, 0.3032895567580801144 ) ) ;
#3388=FACE_OUTER_BOUND ( 'NONE', #15781, .T. ) ;
#3402=AXIS2_PLACEMENT_3D ( 'NONE', #1186, #30279, #8475 ) ;
#3414=VERTEX_POINT ( 'NONE', #31948 ) ;
#3450=ORIENTED_EDGE ( 'NONE', *, *, #35646, .T. ) ;
#3501=CARTESIAN_POINT ( 'NONE',  ( -0.1211759891752730300, -0.5069122841110217381, 0.3093762286737222755 ) ) ;
#3524=AXIS2_PLACEMENT_3D ( 'NONE', #27854, #40175, #8705 ) ;
#3601=CARTESIAN_POINT ( 'NONE',  ( -0.1172401355130441442, -0.4876450271195239550, 0.3356658914665608950 ) ) ;
#3667=CIRCLE ( 'NONE', #26672, 0.06000000000000031697 ) ;
#3690=ORIENTED_EDGE ( 'NONE', *, *, #297, .F. ) ;
#3748=DIRECTION ( 'NONE',  ( -7.771561172376107616E-16, 7.170354002788761615E-17, -1.000000000000000000 ) ) ;
#3755=DIRECTION ( 'NONE',  ( 1.000000000000000000, 0.000000000000000000, 7.847503847416053677E-16 ) ) ;
#3764=CARTESIAN_POINT ( 'NONE',  ( -0.1643313925801952735, 0.5105373599712236254, 0.1162626052509350555 ) ) ;
#3800=CARTESIAN_POINT ( 'NONE',  ( -0.1123064544305908963, -0.5135141720357597750, 0.3236707397771521055 ) ) ;
#3812=CARTESIAN_POINT ( 'NONE',  ( -0.1455608194604302852, -0.5249067277714103419, 0.1528658435937000626 ) ) ;
#3906=EDGE_CURVE ( 'NONE', #7093, #17060, #2142, .T. ) ;
#3907=CARTESIAN_POINT ( 'NONE',  ( -0.1656893171628588957, 0.4813634391809756830, 0.3338433979332086632 ) ) ;
#3908=DIRECTION ( 'NONE',  ( 7.771561172376107616E-16, -7.170354002788761615E-17, 1.000000000000000000 ) ) ;
#3921=ORIENTED_EDGE ( 'NONE', *, *, #5958, .T. ) ;
#3933=CARTESIAN_POINT ( 'NONE',  ( -0.1667768525404892954, 0.4849111360356626044, 0.1246604372685282680 ) ) ;
#4026=DIRECTION ( 'NONE',  ( 1.000000000000000000, 0.000000000000000000, 8.537024980200792236E-16 ) ) ;
#4103=CARTESIAN_POINT ( 'NONE',  ( -0.1608142870582113526, 0.4995150451154150573, 0.3323678566780322585 ) ) ;
#4108=CARTESIAN_POINT ( 'NONE',  ( -0.2789010053595599725, 0.4834754829570393486, 0.09999999999999961697 ) ) ;
#4135=ORIENTED_EDGE ( 'NONE', *, *, #15487, .T. ) ;
#4167=AXIS2_PLACEMENT_3D ( 'NONE', #9114, #5626, #18182 ) ;
#4170=EDGE_CURVE ( 'NONE', #14568, #34195, #18766, .T. ) ;
#4179=ADVANCED_FACE ( 'NONE', ( #8975 ), #40028, .T. ) ;
#4198=CARTESIAN_POINT ( 'NONE',  ( -0.1062892842221209583, -0.4838739999896601307, 0.3472338291022021850 ) ) ;
#4224=VECTOR ( 'NONE', #25585, 39.37007874015748143 ) ;
#4237=CIRCLE ( 'NONE', #29861, 0.01499999999999999771 ) ;
#4349=CARTESIAN_POINT ( 'NONE',  ( -0.1731185243557763487, 0.5373335498847187086, 0.3599999999999993205 ) ) ;
#4351=ORIENTED_EDGE ( 'NONE', *, *, #40586, .F. ) ;
#4359=CARTESIAN_POINT ( 'NONE',  ( -0.1743922129835730472, -0.5166151207188712791, 0.08499999999999964528 ) ) ;
#4393=DIRECTION ( 'NONE',  ( 1.000000000000000000, 1.024442997624095147E-14, 1.138269997360105631E-15 ) ) ;
#4462=CYLINDRICAL_SURFACE ( 'NONE', #29090, 0.9087847906030127598 ) ;
#4506=CARTESIAN_POINT ( 'NONE',  ( -0.1524914371963956017, 0.4722463545162183807, 0.3472338286530394225 ) ) ;
#4517=CARTESIAN_POINT ( 'NONE',  ( -0.1172100234506803368, -0.4874937943216627323, 0.3357378396897046091 ) ) ;
#4602=CARTESIAN_POINT ( 'NONE',  ( -0.2666757540196697529, 0.4921670437878978843, 0.08499999999999936773 ) ) ;
#4617=CARTESIAN_POINT ( 'NONE',  ( -0.09579104668929040722, -0.04310840302197994911, 0.08500000000000008937 ) ) ;
#4644=VECTOR ( 'NONE', #33988, 39.37007874015748143 ) ;
#4670=VERTEX_POINT ( 'NONE', #20271 ) ;
#4676=CARTESIAN_POINT ( 'NONE',  ( -0.1668451997768051753, 0.4851271022253541565, 0.1251051315678503029 ) ) ;
#4691=CARTESIAN_POINT ( 'NONE',  ( -0.2343922129835731560, -0.5166151207188712791, 0.3599999999999990985 ) ) ;
#4699=CARTESIAN_POINT ( 'NONE',  ( -0.1664683893528022818, 0.5171715631282262082, 0.3299773601679611978 ) ) ;
#4713=ORIENTED_EDGE ( 'NONE', *, *, #28764, .F. ) ;
#4767=VERTEX_POINT ( 'NONE', #15090 ) ;
#4818=CYLINDRICAL_SURFACE ( 'NONE', #18672, 0.02999999999999998848 ) ;
#4853=PRODUCT ( 'Parallelogram front_FRONT', 'Parallelogram front_FRONT', '', ( #18344 ) ) ;
#4866=CARTESIAN_POINT ( 'NONE',  ( -2.070754768975505034, -0.09959325338431362917, 0.08499999999999909017 ) ) ;
#4870=CARTESIAN_POINT ( 'NONE',  ( -0.1044460467970230316, -0.4741855622371820567, 0.3602693341844401265 ) ) ;
#4890=CARTESIAN_POINT ( 'NONE',  ( -0.1659602879904918671, 0.5155992160893299037, 0.1238948718127771270 ) ) ;
#4920=EDGE_CURVE ( 'NONE', #9996, #11394, #31916, .T. ) ;
#4941=AXIS2_PLACEMENT_3D ( 'NONE', #2805, #8766, #33880 ) ;
#4951=CARTESIAN_POINT ( 'NONE',  ( -0.1655857493438344097, 0.4810233835288787452, 0.3340284351899789894 ) ) ;
#4981=VERTEX_POINT ( 'NONE', #22500 ) ;
#4986=CARTESIAN_POINT ( 'NONE',  ( -0.09579104668929040722, -0.04310840302197994911, 0.3600000000000000422 ) ) ;
#5036=CARTESIAN_POINT ( 'NONE',  ( -0.1969433606228570832, 0.5138636982738132852, 0.3750000000000001110 ) ) ;
#5051=ORIENTED_EDGE ( 'NONE', *, *, #10049, .T. ) ;
#5128=ORIENTED_EDGE ( 'NONE', *, *, #34424, .F. ) ;
#5193=DIRECTION ( 'NONE',  ( 7.771561172376107616E-16, -7.170354002788761615E-17, 1.000000000000000000 ) ) ;
#5231=DIRECTION ( 'NONE',  ( -7.771561172376107616E-16, 7.170354002788761615E-17, -1.000000000000000000 ) ) ;
#5241=CARTESIAN_POINT ( 'NONE',  ( -0.1743922129835729085, -0.5166151207188712791, 0.3750000000000001110 ) ) ;
#5292=ORIENTED_EDGE ( 'NONE', *, *, #6808, .T. ) ;
#5322=CARTESIAN_POINT ( 'NONE',  ( -0.1092363788443199563, -0.4985689912535452017, 0.1005717796976069445 ) ) ;
#5323=ORIENTED_EDGE ( 'NONE', *, *, #25654, .F. ) ;
#5328=CIRCLE ( 'NONE', #28352, 0.03000000000000022787 ) ;
#5343=DIRECTION ( 'NONE',  ( 1.000000000000000000, -2.276539994720207319E-15, 1.138269997360103659E-15 ) ) ;
#5345=CIRCLE ( 'NONE', #35582, 0.02999999999999999195 ) ;
#5379=AXIS2_PLACEMENT_3D ( 'NONE', #32359, #16752, #29299 ) ;
#5393=DIRECTION ( 'NONE',  ( -7.771561172376107616E-16, 7.170354002788761615E-17, -1.000000000000000000 ) ) ;
#5414=ADVANCED_FACE ( 'NONE', ( #24253 ), #27134, .F. ) ;
#5521=CARTESIAN_POINT ( 'NONE',  ( -0.1642263573060748216, 0.5103503758725048689, 0.3090632479873839378 ) ) ;
#5543=CARTESIAN_POINT ( 'NONE',  ( -0.1062912471183375118, -0.4837944836747087862, 0.1097058945452914075 ) ) ;
#5558=CARTESIAN_POINT ( 'NONE',  ( -0.1630570426857044508, 0.4726602372414858144, 0.3374198529391160273 ) ) ;
#5560=ORIENTED_EDGE ( 'NONE', *, *, #19480, .F. ) ;
#5601=ORIENTED_EDGE ( 'NONE', *, *, #11715, .T. ) ;
#5626=DIRECTION ( 'NONE',  ( 7.771561172376107616E-16, -7.170354002788761615E-17, 1.000000000000000000 ) ) ;
#5680=DIRECTION ( 'NONE',  ( -7.771561172376097755E-16, -7.170354002788760383E-17, 1.000000000000000000 ) ) ;
#5732=CARTESIAN_POINT ( 'NONE',  ( -0.1212185660208173754, -0.5071153786978156441, 0.3078438575813711164 ) ) ;
#5751=CARTESIAN_POINT ( 'NONE',  ( -0.1044436713285770701, -0.4741860147766130962, 0.09550516381870584326 ) ) ;
#5753=CARTESIAN_POINT ( 'NONE',  ( -0.1873388932668320073, 0.5325605939836577374, 0.09999999999999989453 ) ) ;
#5766=CARTESIAN_POINT ( 'NONE',  ( -0.1210148435730253880, -0.5061394519557965710, 0.3122829191278980177 ) ) ;
#5803=CARTESIAN_POINT ( 'NONE',  ( -0.1509132741912886377, 0.4664843738648666305, 0.09813923389061204872 ) ) ;
#5887=ADVANCED_BREP_SHAPE_REPRESENTATION ( '', ( #32046, #27819 ), #33063 ) ;
#5929=EDGE_CURVE ( 'NONE', #1752, #17150, #14234, .T. ) ;
#5949=ORIENTED_EDGE ( 'NONE', *, *, #8061, .T. ) ;
#5958=EDGE_CURVE ( 'NONE', #12799, #51, #14297, .T. ) ;
#5959=CARTESIAN_POINT ( 'NONE',  ( -0.1129900121204312630, -0.5167580615070168637, 0.3146079272632524848 ) ) ;
#6004=CIRCLE ( 'NONE', #3402, 0.9237847906030128842 ) ;
#6044=CARTESIAN_POINT ( 'NONE',  ( -0.08408070219615630669, -0.09959325338431362917, 0.08499999999999756362 ) ) ;
#6081=DIRECTION ( 'NONE',  ( 0.000000000000000000, 0.000000000000000000, -1.000000000000000000 ) ) ;
#6098=CARTESIAN_POINT ( 'NONE',  ( -0.1642263571684416112, 0.5103503754387010982, 0.1528658435937233773 ) ) ;
#6114=CIRCLE ( 'NONE', #25846, 0.03000000000000022787 ) ;
#6152=AXIS2_PLACEMENT_3D ( 'NONE', #3345, #38309, #9529 ) ;
#6153=CARTESIAN_POINT ( 'NONE',  ( -0.1208103506584059517, -0.5051587313117206213, 0.1401839043133220331 ) ) ;
#6186=CIRCLE ( 'NONE', #10127, 0.03000000000000000583 ) ;
#6192=DIRECTION ( 'NONE',  ( -7.771561172376107616E-16, 7.170354002788761615E-17, -1.000000000000000000 ) ) ;
#6319=ORIENTED_EDGE ( 'NONE', *, *, #15310, .T. ) ;
#6331=CIRCLE ( 'NONE', #8328, 0.06000000000000031697 ) ;
#6435=DIRECTION ( 'NONE',  ( -7.771561172376107616E-16, 7.170354002788761615E-17, -1.000000000000000000 ) ) ;
#6450=ORIENTED_EDGE ( 'NONE', *, *, #29933, .T. ) ;
#6475=ADVANCED_FACE ( 'NONE', ( #28028 ), #31341, .T. ) ;
#6526=DIRECTION ( 'NONE',  ( 1.000000000000000000, 1.118011712966791197E-31, -7.771561172376107616E-16 ) ) ;
#6546=ORIENTED_EDGE ( 'NONE', *, *, #28124, .T. ) ;
#6565=CARTESIAN_POINT ( 'NONE',  ( -0.1126900943574665054, -0.5191528599708419289, 0.3032895567580775609 ) ) ;
#6579=VECTOR ( 'NONE', #37421, 39.37007874015748143 ) ;
#6595=ORIENTED_EDGE ( 'NONE', *, *, #27787, .F. ) ;
#6612=AXIS2_PLACEMENT_3D ( 'NONE', #39154, #26406, #17731 ) ;
#6632=CARTESIAN_POINT ( 'NONE',  ( -0.09908070219615711105, -0.09959325338431362917, 0.09550516381870158278 ) ) ;
#6633=AXIS2_PLACEMENT_3D ( 'NONE', #38601, #1984, #14507 ) ;
#6641=AXIS2_PLACEMENT_3D ( 'NONE', #11314, #10709, #14387 ) ;
#6649=ORIENTED_EDGE ( 'NONE', *, *, #1971, .F. ) ;
#6668=CARTESIAN_POINT ( 'NONE',  ( -0.1068374249684608812, -0.4867512985521031954, 0.3606502370888775011 ) ) ;
#6751=DIRECTION ( 'NONE',  ( -1.000000000000000000, 0.000000000000000000, -1.138269997360103659E-15 ) ) ;
#6796=AXIS2_PLACEMENT_3D ( 'NONE', #21607, #39485, #11528 ) ;
#6808=EDGE_CURVE ( 'NONE', #34195, #3414, #29566, .T. ) ;
#6829=CARTESIAN_POINT ( 'NONE',  ( -0.2900000000000002576, 0.5182417262804744906, 0.3599999999999993761 ) ) ;
#6836=DIRECTION ( 'NONE',  ( 7.771561172376107616E-16, -7.170354002788761615E-17, 1.000000000000000000 ) ) ;
#6887=DIRECTION ( 'NONE',  ( 0.000000000000000000, 1.000000000000000000, -2.162712994984206616E-14 ) ) ;
#6986=ORIENTED_EDGE ( 'NONE', *, *, #23131, .F. ) ;
#6989=CIRCLE ( 'NONE', #14210, 2.001558204291726373 ) ;
#6999=CARTESIAN_POINT ( 'NONE',  ( -0.1617502512268864101, 0.4682890762661574557, 0.3382895567546906346 ) ) ;
#7002=DIRECTION ( 'NONE',  ( 7.771561172376107616E-16, -7.170354002788761615E-17, 1.000000000000000000 ) ) ;
#7009=CARTESIAN_POINT ( 'NONE',  ( -0.1212602504878774051, -0.5073146173917495450, 0.3032895567580812246 ) ) ;
#7048=B_SPLINE_CURVE_WITH_KNOTS ( 'NONE', 3,
 ( #11101, #1455, #11707, #8599, #13970, #20366, #4699, #17270, #29823, #30212 ),
 .UNSPECIFIED., .F., .F.,
 ( 4, 2, 2, 2, 4 ),
 ( 0.0002266766535735013997, 0.0007552434839518216026, 0.001283810314330141806, 0.001812377144708462008, 0.002340943975086781995 ),
 .UNSPECIFIED. ) ;
#7073=CARTESIAN_POINT ( 'NONE',  ( -0.1129900121204265445, -0.5167580615070231920, 0.3146079272632528734 ) ) ;
#7093=VERTEX_POINT ( 'NONE', #21608 ) ;
#7175=CARTESIAN_POINT ( 'NONE',  ( -0.1684323895664684156, 0.5231977504175356897, 0.1528658435937000626 ) ) ;
#7201=ADVANCED_FACE ( 'NONE', ( #28782 ), #238, .T. ) ;
#7206=EDGE_LOOP ( 'NONE', ( #7571, #31002, #23075, #5323, #29851, #30850 ) ) ;
#7251=CYLINDRICAL_SURFACE ( 'NONE', #5379, 1.991674066779348218 ) ;
#7272=AXIS2_PLACEMENT_3D ( 'NONE', #20958, #23242, #32871 ) ;
#7350=ORIENTED_EDGE ( 'NONE', *, *, #13486, .F. ) ;
#7381=CARTESIAN_POINT ( 'NONE',  ( -0.1699622337672930805, 0.4951791062278213529, 0.3187362200132102807 ) ) ;
#7383=CARTESIAN_POINT ( 'NONE',  ( -0.1969433606228570832, 0.5138636982738132852, 0.3750000000000001110 ) ) ;
#7384=CIRCLE ( 'NONE', #30399, 0.03000000000000022787 ) ;
#7387=DIRECTION ( 'NONE',  ( 1.000000000000000000, 1.169383359989550442E-31, -7.771561172376108602E-16 ) ) ;
#7429=ORIENTED_EDGE ( 'NONE', *, *, #27753, .T. ) ;
#7462=ORIENTED_EDGE ( 'NONE', *, *, #8783, .T. ) ;
#7467=CARTESIAN_POINT ( 'NONE',  ( -0.1743922129835729085, -0.5166151207188712791, 0.3599999999999990430 ) ) ;
#7522=CYLINDRICAL_SURFACE ( 'NONE', #12776, 2.001674066779348227 ) ;
#7571=ORIENTED_EDGE ( 'NONE', *, *, #38475, .F. ) ;
#7599=AXIS2_PLACEMENT_3D ( 'NONE', #26052, #26441, #11017 ) ;
#7600=CARTESIAN_POINT ( 'NONE',  ( -0.1542173385434465194, 0.4780076866987634232, 0.3460825593793592780 ) ) ;
#7602=DIRECTION ( 'NONE',  ( 1.000000000000000000, 0.000000000000000000, 7.762739824594491602E-16 ) ) ;
#7619=ADVANCED_FACE ( 'NONE', ( #32513 ), #19583, .F. ) ;
#7716=VERTEX_POINT ( 'NONE', #20594 ) ;
#7731=CARTESIAN_POINT ( 'NONE',  ( -0.1450923023275084156, -0.5230583524814751417, 0.1380392329925462791 ) ) ;
#7744=ORIENTED_EDGE ( 'NONE', *, *, #16014, .T. ) ;
#7764=CARTESIAN_POINT ( 'NONE',  ( -0.1049931804392554846, -0.4770575742336289338, 0.3602693336304481075 ) ) ;
#7779=CARTESIAN_POINT ( 'NONE',  ( -0.1603938765018626533, 0.4636889572248046321, 0.1178658435937001703 ) ) ;
#7864=ORIENTED_EDGE ( 'NONE', *, *, #2462, .F. ) ;
#7909=EDGE_CURVE ( 'NONE', #37952, #16265, #24348, .T. ) ;
#7922=ORIENTED_EDGE ( 'NONE', *, *, #2946, .F. ) ;
#7973=CARTESIAN_POINT ( 'NONE',  ( -0.1683868308082348830, 0.4901225108767969241, 0.1298109267597974403 ) ) ;
#7986=DIRECTION ( 'NONE',  ( -7.771561172376107616E-16, 7.170354002788761615E-17, -1.000000000000000000 ) ) ;
#8004=AXIS2_PLACEMENT_3D ( 'NONE', #23588, #20700, #36106 ) ;
#8029=DIRECTION ( 'NONE',  ( -7.771561172376107616E-16, 7.170354002788761615E-17, -1.000000000000000000 ) ) ;
#8036=ORIENTED_EDGE ( 'NONE', *, *, #38776, .T. ) ;
#8061=EDGE_CURVE ( 'NONE', #22311, #8287, #14487, .T. ) ;
#8083=DIRECTION ( 'NONE',  ( -1.000000000000000000, 0.000000000000000000, -7.847494366974319310E-16 ) ) ;
#8131=CARTESIAN_POINT ( 'NONE',  ( -2.070754768975505034, -0.09959325338431362917, 0.3749999999999976130 ) ) ;
#8134=EDGE_LOOP ( 'NONE', ( #5128, #9708, #8671, #19297, #37580, #21829 ) ) ;
#8144=ORIENTED_EDGE ( 'NONE', *, *, #3906, .T. ) ;
#8147=ORIENTED_EDGE ( 'NONE', *, *, #36423, .T. ) ;
#8162=DIRECTION ( 'NONE',  ( -7.771561172376107616E-16, 7.170354002788761615E-17, -1.000000000000000000 ) ) ;
#8186=CARTESIAN_POINT ( 'NONE',  ( -0.1608166228772861250, 0.4995225507410082089, 0.1237952727409504516 ) ) ;
#8261=CARTESIAN_POINT ( 'NONE',  ( -0.2789010053595591954, 0.4834754829570393486, 0.3599999999999987654 ) ) ;
#8287=VERTEX_POINT ( 'NONE', #20148 ) ;
#8315=DIRECTION ( 'NONE',  ( 1.000000000000000000, 0.000000000000000000, 0.000000000000000000 ) ) ;
#8328=AXIS2_PLACEMENT_3D ( 'NONE', #39722, #24121, #5343 ) ;
#8373=PRODUCT_DEFINITION ( 'UNKNOWN', '', #39149, #23669 ) ;
#8384=FACE_OUTER_BOUND ( 'NONE', #16426, .T. ) ;
#8418=ORIENTED_EDGE ( 'NONE', *, *, #30543, .T. ) ;
#8425=EDGE_LOOP ( 'NONE', ( #11538, #12046, #32068, #18233 ) ) ;
#8443=CARTESIAN_POINT ( 'NONE',  ( -0.1710642718812830643, 0.4986889572247752977, 0.3079501053856176784 ) ) ;
#8475=DIRECTION ( 'NONE',  ( 1.000000000000000000, 0.000000000000000000, 8.132394101956133308E-16 ) ) ;
#8482=ORIENTED_EDGE ( 'NONE', *, *, #3906, .F. ) ;
#8484=EDGE_LOOP ( 'NONE', ( #6986, #23792, #21158, #22694, #38130, #31573 ) ) ;
#8489=DIRECTION ( 'NONE',  ( -0.2147743920926303840, -0.9766636885342064867, -4.765223073521777996E-15 ) ) ;
#8549=LINE ( 'NONE', #40446, #31191 ) ;
#8599=CARTESIAN_POINT ( 'NONE',  ( -0.1608542991165615721, 0.4995867522469602529, 0.3503927954982317128 ) ) ;
#8638=ORIENTED_EDGE ( 'NONE', *, *, #27753, .F. ) ;
#8671=ORIENTED_EDGE ( 'NONE', *, *, #39139, .T. ) ;
#8672=LINE ( 'NONE', #40562, #4644 ) ;
#8694=ADVANCED_FACE ( 'NONE', ( #19487 ), #32249, .T. ) ;
#8705=DIRECTION ( 'NONE',  ( 0.9480245940703959651, 0.3181970600707381691, 0.000000000000000000 ) ) ;
#8716=CARTESIAN_POINT ( 'NONE',  ( -0.1455608194604313677, -0.5249067277714107860, 0.3032895567580803919 ) ) ;
#8750=DIRECTION ( 'NONE',  ( -1.000000000000000000, 0.000000000000000000, 0.000000000000000000 ) ) ;
#8766=DIRECTION ( 'NONE',  ( 7.771561172376107616E-16, -7.170354002788761615E-17, 1.000000000000000000 ) ) ;
#8783=EDGE_CURVE ( 'NONE', #4981, #23884, #994, .T. ) ;
#8786=ORIENTED_EDGE ( 'NONE', *, *, #36423, .F. ) ;
#8799=DIRECTION ( 'NONE',  ( 1.000000000000000000, -3.406373435249580326E-19, 7.771561172376097755E-16 ) ) ;
#8803=CIRCLE ( 'NONE', #6152, 0.02999999999999998848 ) ;
#8805=CARTESIAN_POINT ( 'NONE',  ( -0.1044460467970230316, -0.4741855622371820567, 0.3602693341844401265 ) ) ;
#8841=CARTESIAN_POINT ( 'NONE',  ( -0.1196081096344499550, -0.4993394475604064908, 0.1302951649420537872 ) ) ;
#8865=DIRECTION ( 'NONE',  ( -1.000000000000000000, 0.000000000000000000, 0.000000000000000000 ) ) ;
#8920=CARTESIAN_POINT ( 'NONE',  ( 0.000000000000000000, 0.000000000000000000, 0.000000000000000000 ) ) ;
#8942=ORIENTED_EDGE ( 'NONE', *, *, #24100, .T. ) ;
#8954=VERTEX_POINT ( 'NONE', #13515 ) ;
#8957=ORIENTED_EDGE ( 'NONE', *, *, #18808, .F. ) ;
#8973=ADVANCED_FACE ( 'NONE', ( #22979 ), #29355, .F. ) ;
#8975=FACE_OUTER_BOUND ( 'NONE', #23501, .T. ) ;
#8994=ADVANCED_FACE ( 'NONE', ( #21526 ), #17609, .T. ) ;
#9014=ORIENTED_EDGE ( 'NONE', *, *, #13270, .F. ) ;
#9049=CARTESIAN_POINT ( 'NONE',  ( -0.1148699535791894571, -0.5253002637279450271, 0.1262353127152268661 ) ) ;
#9065=VERTEX_POINT ( 'NONE', #30155 ) ;
#9114=CARTESIAN_POINT ( 'NONE',  ( -0.1743922129835733248, -0.5166151207188712791, 0.09999999999999961697 ) ) ;
#9230=ORIENTED_EDGE ( 'NONE', *, *, #11197, .F. ) ;
#9259=ADVANCED_FACE ( 'NONE', ( #24161 ), #21264, .T. ) ;
#9363=AXIS2_PLACEMENT_3D ( 'NONE', #16406, #16016, #34721 ) ;
#9384=CARTESIAN_POINT ( 'NONE',  ( -0.2136509456379319383, -0.4946207598421927254, 0.08499999999999936773 ) ) ;
#9455=CARTESIAN_POINT ( 'NONE',  ( -0.09579104668929040722, -0.04310840302197994911, 0.3749999999999998890 ) ) ;
#9529=DIRECTION ( 'NONE',  ( 1.000000000000000000, 0.000000000000000000, 1.138269997360110167E-15 ) ) ;
#9530=( NAMED_UNIT ( * ) PLANE_ANGLE_UNIT ( ) SI_UNIT ( $, .RADIAN. ) );
#9532=EDGE_CURVE ( 'NONE', #38042, #21695, #2108, .T. ) ;
#9568=ORIENTED_EDGE ( 'NONE', *, *, #10518, .T. ) ;
#9596=VERTEX_POINT ( 'NONE', #4349 ) ;
#9633=DIRECTION ( 'NONE',  ( 7.771561172376107616E-16, -7.170354002788761615E-17, 1.000000000000000000 ) ) ;
#9649=CARTESIAN_POINT ( 'NONE',  ( -0.1743922129835729085, -0.5166151207188712791, 0.3750000000000001110 ) ) ;
#9663=CARTESIAN_POINT ( 'NONE',  ( -0.1059790098053068758, -0.4816261856389994489, 0.09813923389061053604 ) ) ;
#9708=ORIENTED_EDGE ( 'NONE', *, *, #38475, .T. ) ;
#9709=VERTEX_POINT ( 'NONE', #5766 ) ;
#9713=ORIENTED_EDGE ( 'NONE', *, *, #39876, .F. ) ;
#9719=EDGE_CURVE ( 'NONE', #38543, #12918, #2736, .T. ) ;
#9750=ORIENTED_EDGE ( 'NONE', *, *, #1971, .T. ) ;
#9756=EDGE_CURVE ( 'NONE', #8954, #35941, #5345, .T. ) ;
#9799=DIRECTION ( 'NONE',  ( 7.771561172376107616E-16, -7.170354002788761615E-17, 1.000000000000000000 ) ) ;
#9803=DIRECTION ( 'NONE',  ( -1.000000000000000000, 9.772892703439654860E-15, -7.801168736956215639E-16 ) ) ;
#9902=EDGE_LOOP ( 'NONE', ( #8957, #18781, #20359, #38008 ) ) ;
#9910=CARTESIAN_POINT ( 'NONE',  ( -0.1696282724551476662, 0.4941130859153646249, 0.1349535128744427936 ) ) ;
#9929=LENGTH_MEASURE_WITH_UNIT ( LENGTH_MEASURE( 0.02539999999999999897 ), #21282 );
#9937=ADVANCED_FACE ( 'NONE', ( #21827 ), #25843, .T. ) ;
#9957=CARTESIAN_POINT ( 'NONE',  ( -2.070754768975505034, -0.09959325338431362917, 0.09550516381870004234 ) ) ;
#9972=CARTESIAN_POINT ( 'NONE',  ( -0.1196127869351431838, -0.4993621520964605653, 0.3258261256381336235 ) ) ;
#9996=VERTEX_POINT ( 'NONE', #13577 ) ;
#10008=CARTESIAN_POINT ( 'NONE',  ( -0.1443922129835726875, -0.5166151207188712791, 0.3750000000000001110 ) ) ;
#10033=CARTESIAN_POINT ( 'NONE',  ( -1.019575837292303166, -0.04310840302197994911, 0.09999999999999879818 ) ) ;
#10049=EDGE_CURVE ( 'NONE', #29582, #31816, #30968, .T. ) ;
#10085=CIRCLE ( 'NONE', #271, 0.03000000000000002318 ) ;
#10089=CARTESIAN_POINT ( 'NONE',  ( -0.1603938765018590729, 0.4636889572247935298, 0.3382895567580809226 ) ) ;
#10110=CARTESIAN_POINT ( 'NONE',  ( -0.2136509456379319383, -0.4946207598421927254, 0.3749999999999995559 ) ) ;
#10127=AXIS2_PLACEMENT_3D ( 'NONE', #7731, #39600, #11435 ) ;
#10163=CIRCLE ( 'NONE', #28555, 1.991674066779348218 ) ;
#10182=CARTESIAN_POINT ( 'NONE',  ( -0.1124400704934240963, -0.5139941482048617782, 0.3450122074418745521 ) ) ;
#10222=CARTESIAN_POINT ( 'NONE',  ( -2.070754768975505034, -0.09959325338431362917, 0.09999999999999933942 ) ) ;
#10308=CARTESIAN_POINT ( 'NONE',  ( -0.1638575715552355871, 0.5090525736529738499, 0.3414257732885147556 ) ) ;
#10311=FACE_OUTER_BOUND ( 'NONE', #30779, .T. ) ;
#10349=CARTESIAN_POINT ( 'NONE',  ( -0.1574377185082707353, 0.4885537809602777948, 0.09999999999999989453 ) ) ;
#10420=CARTESIAN_POINT ( 'NONE',  ( -0.1533385355407297923, 0.4750492940987078860, 0.3599999999999995981 ) ) ;
#10503=CARTESIAN_POINT ( 'NONE',  ( -0.1443922129835728263, -0.5166151207188712791, 0.08499999999999961753 ) ) ;
#10504=EDGE_LOOP ( 'NONE', ( #1757, #31120, #6319, #7864 ) ) ;
#10509=ORIENTED_EDGE ( 'NONE', *, *, #18086, .T. ) ;
#10518=EDGE_CURVE ( 'NONE', #4981, #29632, #34973, .T. ) ;
#10542=LINE ( 'NONE', #19203, #4224 ) ;
#10559=ORIENTED_EDGE ( 'NONE', *, *, #33818, .T. ) ;
#10561=AXIS2_PLACEMENT_3D ( 'NONE', #10222, #9799, #16201 ) ;
#10576=ORIENTED_EDGE ( 'NONE', *, *, #36088, .T. ) ;
#10585=AXIS2_PLACEMENT_3D ( 'NONE', #30828, #11704, #33489 ) ;
#10586=CARTESIAN_POINT ( 'NONE',  ( -2.070754768975505034, -0.09959325338431362917, 0.09813923389047245205 ) ) ;
#10588=AXIS2_PLACEMENT_3D ( 'NONE', #5241, #34242, #12252 ) ;
#10631=ORIENTED_EDGE ( 'NONE', *, *, #21600, .T. ) ;
#10667=CARTESIAN_POINT ( 'NONE',  ( -0.1566201954065875035, 0.4859225043295781199, 0.1133527062597455004 ) ) ;
#10683=CARTESIAN_POINT ( 'NONE',  ( -0.1167294259372883281, -0.5331983348239499598, 0.3084771640796409864 ) ) ;
#10695=CARTESIAN_POINT ( 'NONE',  ( -0.1126900943574664637, -0.5191528599708425951, 0.1528658435936960103 ) ) ;
#10703=CARTESIAN_POINT ( 'NONE',  ( -0.1743922129835730472, -0.5166151207188712791, 0.08499999999999964528 ) ) ;
#10709=DIRECTION ( 'NONE',  ( -7.771561172376107616E-16, 7.170354002788761615E-17, -1.000000000000000000 ) ) ;
#10766=ADVANCED_FACE ( 'NONE', ( #26709 ), #4462, .F. ) ;
#10782=LINE ( 'NONE', #23553, #20677 ) ;
#10838=VERTEX_POINT ( 'NONE', #16835 ) ;
#10875=TOROIDAL_SURFACE ( 'NONE', #27305, 0.04500000000000032446, 0.01499999999999999944 ) ;
#10885=CARTESIAN_POINT ( 'NONE',  ( -0.1574073192761738238, 0.4884966930314057487, 0.1147307106484463379 ) ) ;
#10967=LENGTH_MEASURE_WITH_UNIT ( LENGTH_MEASURE( 0.02539999999999999897 ), #38919 );
#10990=ORIENTED_EDGE ( 'NONE', *, *, #34115, .F. ) ;
#11017=DIRECTION ( 'NONE',  ( 1.000000000000000000, 0.000000000000000000, 7.847494366974321282E-16 ) ) ;
#11082=CARTESIAN_POINT ( 'NONE',  ( -0.1595531559346400341, 0.4954596757340542501, 0.1197284696570148632 ) ) ;
#11101=CARTESIAN_POINT ( 'NONE',  ( -0.1533385355407297923, 0.4750492940987078860, 0.3599999999999995981 ) ) ;
#11104=CARTESIAN_POINT ( 'NONE',  ( -0.1167294258595701767, -0.5331983345537089081, 0.1478951491071181235 ) ) ;
#11181=ORIENTED_EDGE ( 'NONE', *, *, #34424, .T. ) ;
#11197=EDGE_CURVE ( 'NONE', #23884, #35323, #38274, .T. ) ;
#11206=ORIENTED_EDGE ( 'NONE', *, *, #33015, .F. ) ;
#11213=VECTOR ( 'NONE', #34709, 39.37007874015748143 ) ;
#11222=DIRECTION ( 'NONE',  ( -1.000000000000000000, 0.000000000000000000, -7.847494366974319310E-16 ) ) ;
#11223=DIRECTION ( 'NONE',  ( 1.000000000000000000, 0.000000000000000000, 8.537024980200777445E-16 ) ) ;
#11301=CARTESIAN_POINT ( 'NONE',  ( -0.1127636766158876952, -0.5184084763139977792, 0.1453728055589495471 ) ) ;
#11314=CARTESIAN_POINT ( 'NONE',  ( -1.019575837292303166, -0.04310840302197994911, 0.09999999999999879818 ) ) ;
#11394=VERTEX_POINT ( 'NONE', #15007 ) ;
#11399=( GEOMETRIC_REPRESENTATION_CONTEXT ( 3 ) GLOBAL_UNCERTAINTY_ASSIGNED_CONTEXT ( ( #15737 ) ) GLOBAL_UNIT_ASSIGNED_CONTEXT ( ( #1126, #26195, #23112 ) ) REPRESENTATION_CONTEXT ( 'NONE', 'WORKASPACE' ) );
#11410=DIRECTION ( 'NONE',  ( -7.771561172376107616E-16, 7.170354002788761615E-17, -1.000000000000000000 ) ) ;
#11435=DIRECTION ( 'NONE',  ( -1.309010496964125854E-14, 0.9672079024885572585, 0.2539859708009193917 ) ) ;
#11455=DIRECTION ( 'NONE',  ( -7.771561172376107616E-16, 7.170354002788761615E-17, -1.000000000000000000 ) ) ;
#11490=CARTESIAN_POINT ( 'NONE',  ( -0.1696269498702763501, 0.4941072959623512562, 0.1354043093116702456 ) ) ;
#11528=DIRECTION ( 'NONE',  ( 0.8724162812079783169, -0.4887635750372991139, 0.000000000000000000 ) ) ;
#11538=ORIENTED_EDGE ( 'NONE', *, *, #39139, .F. ) ;
#11658=( BOUNDED_SURFACE ( )  B_SPLINE_SURFACE ( 3, 2, ( 
 ( #13949, #29591, #7779 ),
 ( #30195, #32868, #1435 ),
 ( #29401, #38838, #2026 ),
 ( #39054, #10667, #14555 ),
 ( #27123, #10885, #35973 ),
 ( #26919, #20348, #4676 ),
 ( #39259, #11082, #23643 ),
 ( #36163, #8186, #7973 ),
 ( #33080, #17457, #20760 ),
 ( #4890, #30006, #11490 ),
 ( #24055, #36581, #20952 ),
 ( #40476, #40259, #21372 ),
 ( #18455, #2629, #12299 ),
 ( #34091, #6098, #18061 ) ),
 .UNSPECIFIED., .F., .F., .F. ) 
 B_SPLINE_SURFACE_WITH_KNOTS ( ( 4, 2, 2, 2, 2, 2, 4 ),
 ( 3, 3 ),
 ( 0.001271275560265211274, 0.001846161198739981746, 0.002133604017977366873, 0.002421046837214752001, 0.002708489656452137129, 0.002995932475689522256, 0.003570818114164292512 ),
 ( 0.000000000000000000, 1.000000000000000000 ),
 .UNSPECIFIED. ) 
 GEOMETRIC_REPRESENTATION_ITEM ( )  RATIONAL_B_SPLINE_SURFACE ( (
 ( 1.000000000000000000, 0.9128709291752991062, 1.000000000000000000),
 ( 1.000000000000000000, 0.9128716273348083110, 1.000000000000000000),
 ( 1.000000000000000000, 0.9128126260589567442, 1.000000000000000000),
 ( 1.000000000000000000, 0.9126599423561904123, 1.000000000000000000),
 ( 1.000000000000000000, 0.9125975471392260285, 1.000000000000000000),
 ( 1.000000000000000000, 0.9124617177697034176, 1.000000000000000000),
 ( 1.000000000000000000, 0.9123879986973735257, 1.000000000000000000),
 ( 1.000000000000000000, 0.9122366710451426108, 1.000000000000000000),
 ( 1.000000000000000000, 0.9121592624379696312, 1.000000000000000000),
 ( 1.000000000000000000, 0.9120163032376081835, 1.000000000000000000),
 ( 1.000000000000000000, 0.9119498413177286045, 1.000000000000000000),
 ( 1.000000000000000000, 0.9117793221099002032, 1.000000000000000000),
 ( 1.000000000000000000, 0.9117124009648843730, 1.000000000000000000),
 ( 1.000000000000000000, 0.9117127123830554014, 1.000000000000000000) ) ) 
 REPRESENTATION_ITEM ( '' )  SURFACE ( )  );
#11704=DIRECTION ( 'NONE',  ( 0.2828184691483936475, -0.9591734532964092397, 4.074771315709934095E-15 ) ) ;
#11707=CARTESIAN_POINT ( 'NONE',  ( -0.1572280491643743283, 0.4879031095700123721, 0.3568535915792940827 ) ) ;
#11715=EDGE_CURVE ( 'NONE', #15152, #4767, #29770, .T. ) ;
#11728=CARTESIAN_POINT ( 'NONE',  ( -0.1171721259116252079, -0.4872713820691122466, 0.1209876223252399491 ) ) ;
#11751=CARTESIAN_POINT ( 'NONE',  ( -0.1167294259372891468, -0.5331983348239500708, 0.1528658435937000626 ) ) ;
#11755=LINE ( 'NONE', #30080, #36953 ) ;
#11756=EDGE_CURVE ( 'NONE', #12799, #35807, #36342, .T. ) ;
#11778=ORIENTED_EDGE ( 'NONE', *, *, #5958, .F. ) ;
#11779=EDGE_CURVE ( 'NONE', #40488, #21878, #20346, .T. ) ;
#11816=ORIENTED_EDGE ( 'NONE', *, *, #8783, .F. ) ;
#11831=ORIENTED_EDGE ( 'NONE', *, *, #7909, .F. ) ;
#11895=ORIENTED_EDGE ( 'NONE', *, *, #28764, .T. ) ;
#11905=LINE ( 'NONE', #24083, #19366 ) ;
#11924=DIRECTION ( 'NONE',  ( 0.9480245940703959651, 0.3181970600707381691, 1.138269997360108787E-15 ) ) ;
#11997=CARTESIAN_POINT ( 'NONE',  ( -0.1157923916715208196, -0.5295015842444287246, 0.1380392329925462791 ) ) ;
#12036=AXIS2_PLACEMENT_3D ( 'NONE', #9649, #13336, #13127 ) ;
#12046=ORIENTED_EDGE ( 'NONE', *, *, #39296, .T. ) ;
#12137=CARTESIAN_POINT ( 'NONE',  ( -0.1157351208611892279, -0.4799584063719126159, 0.1184929141221668786 ) ) ;
#12146=ORIENTED_EDGE ( 'NONE', *, *, #1321, .F. ) ;
#12165=CARTESIAN_POINT ( 'NONE',  ( -0.1102510911460810039, -0.5035121463812862741, 0.3528822442262277148 ) ) ;
#12252=DIRECTION ( 'NONE',  ( -1.000000000000000000, 0.000000000000000000, -1.138269997360105631E-15 ) ) ;
#12299=CARTESIAN_POINT ( 'NONE',  ( -0.1710642717957994163, 0.4986889573705637346, 0.1482573527501111488 ) ) ;
#12321=CARTESIAN_POINT ( 'NONE',  ( -0.2600000000000002309, 0.5182417262804744906, 0.3749999999999995559 ) ) ;
#12340=CARTESIAN_POINT ( 'NONE',  ( -0.1204846181304661118, -0.5035940506942929717, 0.1366987775887355816 ) ) ;
#12364=DIRECTION ( 'NONE',  ( 1.000000000000000000, 9.106159978880829274E-15, 1.138269997360103659E-15 ) ) ;
#12447=DIRECTION ( 'NONE',  ( -7.771561172376107616E-16, 7.170354002788761615E-17, -1.000000000000000000 ) ) ;
#12448=EDGE_CURVE ( 'NONE', #23678, #10838, #31130, .T. ) ;
#12474=CARTESIAN_POINT ( 'NONE',  ( -0.1603938765018562418, 0.4636889572247986369, 0.3382895567582878127 ) ) ;
#12529=AXIS2_PLACEMENT_3D ( 'NONE', #7467, #20046, #4393 ) ;
#12613=AXIS2_PLACEMENT_3D ( 'NONE', #7383, #17069, #16276 ) ;
#12614=CARTESIAN_POINT ( 'NONE',  ( -0.1669433606228599432, 0.5138636982738132852, 0.3032895567580801144 ) ) ;
#12652=TOROIDAL_SURFACE ( 'NONE', #9363, 0.9237847906030132172, 0.01499999999999999944 ) ;
#12736=DIRECTION ( 'NONE',  ( -7.771561172376107616E-16, 7.170354002788761615E-17, -1.000000000000000000 ) ) ;
#12775=CARTESIAN_POINT ( 'NONE',  ( -0.1669433606228570843, 0.5138636982738132852, 0.3750000000000001110 ) ) ;
#12776=AXIS2_PLACEMENT_3D ( 'NONE', #8131, #1585, #11222 ) ;
#12789=DIRECTION ( 'NONE',  ( 7.771561172376107616E-16, -7.170354002788761615E-17, 1.000000000000000000 ) ) ;
#12799=VERTEX_POINT ( 'NONE', #20142 ) ;
#12803=DIRECTION ( 'NONE',  ( -1.000000000000000000, 0.000000000000000000, 0.000000000000000000 ) ) ;
#12819=DIRECTION ( 'NONE',  ( 1.000000000000000000, 1.113825344428167933E-31, -7.771561172376107616E-16 ) ) ;
#12828=CIRCLE ( 'NONE', #33852, 0.01499999999999998036 ) ;
#12835=DIRECTION ( 'NONE',  ( -1.000000000000000000, 0.000000000000000000, 0.000000000000000000 ) ) ;
#12848=ORIENTED_EDGE ( 'NONE', *, *, #21002, .T. ) ;
#12861=ORIENTED_EDGE ( 'NONE', *, *, #14962, .F. ) ;
#12868=CARTESIAN_POINT ( 'NONE',  ( -0.1044436713285736007, -0.4741860147766045475, 0.3472338286680813901 ) ) ;
#12879=DIRECTION ( 'NONE',  ( -7.771561172376107616E-16, 7.170354002788761615E-17, -1.000000000000000000 ) ) ;
#12918=VERTEX_POINT ( 'NONE', #12474 ) ;
#12936=AXIS2_PLACEMENT_3D ( 'NONE', #15130, #14737, #33446 ) ;
#12958=VERTEX_POINT ( 'NONE', #15766 ) ;
#12974=ORIENTED_EDGE ( 'NONE', *, *, #11715, .F. ) ;
#12993=DIRECTION ( 'NONE',  ( -1.000000000000000000, 0.000000000000000000, -5.691349986800505477E-16 ) ) ;
#13023=CARTESIAN_POINT ( 'NONE',  ( -0.1684323895664708859, 0.5231977504175450155, 0.1471384328909202122 ) ) ;
#13111=ORIENTED_EDGE ( 'NONE', *, *, #24547, .T. ) ;
#13127=DIRECTION ( 'NONE',  ( 1.000000000000000000, 0.000000000000000000, 1.517693329813472072E-15 ) ) ;
#13188=ADVANCED_FACE ( 'NONE', ( #33014 ), #4818, .T. ) ;
#13197=CARTESIAN_POINT ( 'NONE',  ( -0.1630577892338991308, 0.4726628520879619377, 0.1187338422647633285 ) ) ;
#13226=CIRCLE ( 'NONE', #7272, 1.986674066779348102 ) ;
#13237=TOROIDAL_SURFACE ( 'NONE', #27049, 1.971674066779348866, 0.02999999999999999889 ) ;
#13265=UNCERTAINTY_MEASURE_WITH_UNIT (LENGTH_MEASURE( 1.000000000000000082E-05 ), #925, 'distance_accuracy_value', 'NONE');
#13270=EDGE_CURVE ( 'NONE', #17150, #7093, #21091, .T. ) ;
#13325=AXIS2_PLACEMENT_3D ( 'NONE', #10703, #29835, #1275 ) ;
#13336=DIRECTION ( 'NONE',  ( 7.771561172376107616E-16, -7.170354002788761615E-17, 1.000000000000000000 ) ) ;
#13351=CARTESIAN_POINT ( 'NONE',  ( -0.1088121136105147380, -0.4964308608213456875, 0.09999999999999989453 ) ) ;
#13376=CARTESIAN_POINT ( 'NONE',  ( -0.1613941814439381617, 0.5013693833954199208, 0.3301047373962386899 ) ) ;
#13399=DIRECTION ( 'NONE',  ( -3.406373435249024214E-19, -1.000000000000000000, -7.170354002788761615E-17 ) ) ;
#13418=CARTESIAN_POINT ( 'NONE',  ( -2.070754768975505034, -0.09959325338431362917, 0.09550516381870004234 ) ) ;
#13441=TOROIDAL_SURFACE ( 'NONE', #18702, 0.04500000000000023426, 0.01499999999999999944 ) ;
#13471=CARTESIAN_POINT ( 'NONE',  ( -0.1081899703030904242, -0.4934552128793911474, 0.3439540350797880564 ) ) ;
#13482=DIRECTION ( 'NONE',  ( -6.217248937900885304E-15, 2.158931604386568927E-14, 1.000000000000000000 ) ) ;
#13486=EDGE_CURVE ( 'NONE', #16489, #27939, #20001, .T. ) ;
#13515=CARTESIAN_POINT ( 'NONE',  ( -0.1045574869087414066, -0.4741643323009803734, 0.09813923389047436718 ) ) ;
#13573=CARTESIAN_POINT ( 'NONE',  ( -0.1508044614562676355, 0.4665164580004940720, 0.3602693336111434941 ) ) ;
#13577=CARTESIAN_POINT ( 'NONE',  ( -0.2267371898560524290, -0.4872893062166330780, 0.09999999999999989453 ) ) ;
#13580=AXIS2_PLACEMENT_3D ( 'NONE', #15912, #331, #12835 ) ;
#13593=AXIS2_PLACEMENT_3D ( 'NONE', #24534, #12789, #27612 ) ;
#13673=DIRECTION ( 'NONE',  ( -1.000000000000000000, 0.000000000000000000, -7.762644838731319154E-16 ) ) ;
#13701=ADVANCED_FACE ( 'NONE', ( #27153 ), #375, .T. ) ;
#13702=CARTESIAN_POINT ( 'NONE',  ( -0.1530296545635675409, 0.4740172026173952724, 0.3600612075995228700 ) ) ;
#13771=CARTESIAN_POINT ( 'NONE',  ( -0.1659631349965107749, 0.5156080474714448414, 0.3322463110352368298 ) ) ;
#13772=CARTESIAN_POINT ( 'NONE',  ( -0.1157923916714435481, -0.5295015842440792264, 0.1380392329925451689 ) ) ;
#13867=AXIS2_PLACEMENT_3D ( 'NONE', #25973, #13399, #19586 ) ;
#13878=B_SPLINE_CURVE_WITH_KNOTS ( 'NONE', 3,
 ( #18221, #24397, #2791, #27682 ),
 .UNSPECIFIED., .F., .F.,
 ( 4, 4 ),
 ( 2.088448796179171202E-15, 0.0003951776346070152404 ),
 .UNSPECIFIED. ) ;
#13909=EDGE_CURVE ( 'NONE', #36405, #14568, #11905, .T. ) ;
#13917=EDGE_CURVE ( 'NONE', #26889, #28266, #2860, .T. ) ;
#13932=AXIS2_PLACEMENT_3D ( 'NONE', #10586, #35897, #13673 ) ;
#13949=CARTESIAN_POINT ( 'NONE',  ( -0.1508021419688887199, 0.4665171419162565392, 0.09550516381870571836 ) ) ;
#13963=CARTESIAN_POINT ( 'NONE',  ( -0.1163196563843198195, -0.5318992644065131392, 0.3135508459095567302 ) ) ;
#13970=CARTESIAN_POINT ( 'NONE',  ( -0.1625122179509601028, 0.5048329626761722810, 0.3461446680885716387 ) ) ;
#14137=DIRECTION ( 'NONE',  ( -3.406373435249024214E-19, -1.000000000000000000, -7.170354002788761615E-17 ) ) ;
#14185=CARTESIAN_POINT ( 'NONE',  ( -0.1743922129835729085, -0.5166151207188712791, 0.3750000000000001110 ) ) ;
#14201=ORIENTED_EDGE ( 'NONE', *, *, #17808, .F. ) ;
#14210=AXIS2_PLACEMENT_3D ( 'NONE', #34638, #6435, #31539 ) ;
#14234=CIRCLE ( 'NONE', #24763, 0.02999999999999998848 ) ;
#14275=CARTESIAN_POINT ( 'NONE',  ( -0.1155415985277060270, -0.5283611291160981160, 0.1337613384747759759 ) ) ;
#14297=LINE ( 'NONE', #26857, #37227 ) ;
#14387=DIRECTION ( 'NONE',  ( 1.000000000000000000, 2.043171224247294526E-14, 7.702990362679453920E-16 ) ) ;
#14466=ORIENTED_EDGE ( 'NONE', *, *, #22315, .T. ) ;
#14483=DIRECTION ( 'NONE',  ( 7.771561172376107616E-16, -7.170354002788761615E-17, 1.000000000000000000 ) ) ;
#14487=CIRCLE ( 'NONE', #23064, 0.01499999999999999944 ) ;
#14493=ORIENTED_EDGE ( 'NONE', *, *, #9719, .T. ) ;
#14497=EDGE_CURVE ( 'NONE', #37952, #15629, #18744, .T. ) ;
#14507=DIRECTION ( 'NONE',  ( 1.000000000000000000, 0.000000000000000000, 7.762195515159383243E-16 ) ) ;
#14514=CARTESIAN_POINT ( 'NONE',  ( -0.1142670043590670731, -0.4723146173917492918, 0.1178658435937000315 ) ) ;
#14544=FACE_OUTER_BOUND ( 'NONE', #39454, .T. ) ;
#14555=CARTESIAN_POINT ( 'NONE',  ( -0.1650539334306601047, 0.4792632177816724126, 0.1214379789123969933 ) ) ;
#14568=VERTEX_POINT ( 'NONE', #40193 ) ;
#14582=DIRECTION ( 'NONE',  ( 1.000000000000000000, 1.373428330785184770E-31, -7.771561172376108602E-16 ) ) ;
#14737=DIRECTION ( 'NONE',  ( 7.771561172376107616E-16, -7.170354002788761615E-17, 1.000000000000000000 ) ) ;
#14747=DIRECTION ( 'NONE',  ( -1.000000000000000000, 0.000000000000000000, 0.000000000000000000 ) ) ;
#14752=EDGE_CURVE ( 'NONE', #34195, #19133, #25328, .T. ) ;
#14800=CARTESIAN_POINT ( 'NONE',  ( -1.019575837292303166, -0.04310840302197994911, 0.09999999999999879818 ) ) ;
#14819=CARTESIAN_POINT ( 'NONE',  ( -0.1081053389377021196, -0.4929871184168310161, 0.1128267017629508567 ) ) ;
#14820=ORIENTED_EDGE ( 'NONE', *, *, #19696, .T. ) ;
#14841=CIRCLE ( 'NONE', #35221, 0.01499999999999999424 ) ;
#14850=DIRECTION ( 'NONE',  ( -7.771561172376107616E-16, 7.170354002788761615E-17, -1.000000000000000000 ) ) ;
#14864=CIRCLE ( 'NONE', #36567, 0.9087847906030128708 ) ;
#14962=EDGE_CURVE ( 'NONE', #9596, #16265, #8672, .T. ) ;
#15007=CARTESIAN_POINT ( 'NONE',  ( -0.2343922129835735724, -0.5166151207188712791, 0.09999999999999967248 ) ) ;
#15026=DIRECTION ( 'NONE',  ( -7.771561172376107616E-16, 7.170354002788761615E-17, -1.000000000000000000 ) ) ;
#15090=CARTESIAN_POINT ( 'NONE',  ( -0.1304423469995336093, -0.5262799683630393632, 0.3749999999999998335 ) ) ;
#15130=CARTESIAN_POINT ( 'NONE',  ( -2.070754768975505034, -0.09959325338431362917, 0.09999999999999933942 ) ) ;
#15152=VERTEX_POINT ( 'NONE', #10110 ) ;
#15177=CARTESIAN_POINT ( 'NONE',  ( -0.1743922129835729085, -0.5166151207188712791, 0.3750000000000001110 ) ) ;
#15213=CARTESIAN_POINT ( 'NONE',  ( -0.1089540792635268068, -0.4972110540766704889, 0.1150843967103426929 ) ) ;
#15244=CARTESIAN_POINT ( 'NONE',  ( -0.1151536691905419157, -0.5265970617445885349, 0.3290111518013588143 ) ) ;
#15257=TOROIDAL_SURFACE ( 'NONE', #2105, 0.9237847906030132172, 0.01499999999999999944 ) ;
#15267=CIRCLE ( 'NONE', #32318, 0.03000000000000022787 ) ;
#15310=EDGE_CURVE ( 'NONE', #9709, #51, #32904, .T. ) ;
#15333=ORIENTED_EDGE ( 'NONE', *, *, #10518, .F. ) ;
#15337=CARTESIAN_POINT ( 'NONE',  ( -0.2136509456379322158, -0.4946207598421927254, 0.3599999999999998757 ) ) ;
#15466=DIRECTION ( 'NONE',  ( -7.771561172376107616E-16, 7.170354002788761615E-17, -1.000000000000000000 ) ) ;
#15487=EDGE_CURVE ( 'NONE', #26211, #15711, #31691, .T. ) ;
#15501=CARTESIAN_POINT ( 'NONE',  ( -0.1304423469995336093, -0.5262799683630393632, 0.08500000000000018652 ) ) ;
#15560=FACE_OUTER_BOUND ( 'NONE', #19662, .T. ) ;
#15581=CARTESIAN_POINT ( 'NONE',  ( -2.070754768975505034, -0.09959325338431362917, 0.3606502365330779836 ) ) ;
#15629=VERTEX_POINT ( 'NONE', #6044 ) ;
#15630=CARTESIAN_POINT ( 'NONE',  ( -0.1210148435730069999, -0.5061394519556974281, 0.1438724812235067374 ) ) ;
#15644=CARTESIAN_POINT ( 'NONE',  ( -0.1167294260180219145, -0.5331983351046741815, 0.3082670712250488720 ) ) ;
#15653=CARTESIAN_POINT ( 'NONE',  ( -0.1071618391680910221, -0.4882221650595575113, 0.3591756789878951528 ) ) ;
#15689=DIRECTION ( 'NONE',  ( 7.771561172376107616E-16, -7.170354002788761615E-17, 1.000000000000000000 ) ) ;
#15711=VERTEX_POINT ( 'NONE', #37514 ) ;
#15737=UNCERTAINTY_MEASURE_WITH_UNIT (LENGTH_MEASURE( 1.000000000000000082E-05 ), #1126, 'distance_accuracy_value', 'NONE');
#15766=CARTESIAN_POINT ( 'NONE',  ( -0.07908070219615623286, -0.09959325338431362917, 0.1178658435936968396 ) ) ;
#15769=DIRECTION ( 'NONE',  ( -1.252096997096122269E-14, -0.9672079024912928480, 0.2539859707905023356 ) ) ;
#15776=CARTESIAN_POINT ( 'NONE',  ( -0.1157923916715208196, -0.5295015842444287246, 0.3181161673586317962 ) ) ;
#15781=EDGE_LOOP ( 'NONE', ( #26953, #21423, #15940, #27828, #1601 ) ) ;
#15819=TOROIDAL_SURFACE ( 'NONE', #21726, 1.971674066779348866, 0.02999999999999999889 ) ;
#15881=EDGE_LOOP ( 'NONE', ( #35929, #7744 ) ) ;
#15904=AXIS2_PLACEMENT_3D ( 'NONE', #3109, #18330, #12364 ) ;
#15912=CARTESIAN_POINT ( 'NONE',  ( -0.1743922129835729085, -0.5166151207188712791, 0.3750000000000001110 ) ) ;
#15925=ADVANCED_FACE ( 'NONE', ( #739 ), #7251, .T. ) ;
#15936=ORIENTED_EDGE ( 'NONE', *, *, #28124, .F. ) ;
#15940=ORIENTED_EDGE ( 'NONE', *, *, #15310, .F. ) ;
#16014=EDGE_CURVE ( 'NONE', #39656, #26889, #15267, .T. ) ;
#16016=DIRECTION ( 'NONE',  ( 7.771561172376107616E-16, -7.170354002788761615E-17, 1.000000000000000000 ) ) ;
#16100=EDGE_LOOP ( 'NONE', ( #2882, #11181, #8147, #23232, #17416, #3450 ) ) ;
#16149=ORIENTED_EDGE ( 'NONE', *, *, #31387, .T. ) ;
#16169=CARTESIAN_POINT ( 'NONE',  ( -0.1105109110478532802, -0.5048634036869349417, 0.3351973644282389420 ) ) ;
#16201=DIRECTION ( 'NONE',  ( 1.000000000000000000, 1.113825344428167933E-31, -7.771561172376107616E-16 ) ) ;
#16211=VERTEX_POINT ( 'NONE', #26781 ) ;
#16227=CARTESIAN_POINT ( 'NONE',  ( -0.1210148435730033917, -0.5061394519556894345, 0.1438724812234795092 ) ) ;
#16248=ADVANCED_FACE ( 'NONE', ( #50 ), #21199, .T. ) ;
#16265=VERTEX_POINT ( 'NONE', #24494 ) ;
#16276=DIRECTION ( 'NONE',  ( 1.000000000000000000, 0.000000000000000000, 0.000000000000000000 ) ) ;
#16282=DIRECTION ( 'NONE',  ( -7.771561172376107616E-16, 7.170354002788761615E-17, -1.000000000000000000 ) ) ;
#16356=CARTESIAN_POINT ( 'NONE',  ( -0.1204800139379097468, -0.5035717010276847816, 0.3194901984145592233 ) ) ;
#16405=DIRECTION ( 'NONE',  ( 1.000000000000000000, 0.000000000000000000, 7.762195515159383243E-16 ) ) ;
#16406=CARTESIAN_POINT ( 'NONE',  ( -1.019575837292303166, -0.04310840302197994911, 0.3599999999999993205 ) ) ;
#16426=EDGE_LOOP ( 'NONE', ( #39371, #458, #21527, #28222, #1112, #4351 ) ) ;
#16431=DIRECTION ( 'NONE',  ( 0.9766636885342071528, -0.2147743920926261929, 1.138269997360109773E-15 ) ) ;
#16462=CARTESIAN_POINT ( 'NONE',  ( -0.1593715683900499003, 0.4948507460962193183, 0.3535463917166182246 ) ) ;
#16489=VERTEX_POINT ( 'NONE', #9455 ) ;
#16559=VECTOR ( 'NONE', #12447, 39.37007874015748143 ) ;
#16602=CARTESIAN_POINT ( 'NONE',  ( -1.019575837292303166, -0.04310840302197994911, 0.3599999999999993205 ) ) ;
#16668=CARTESIAN_POINT ( 'NONE',  ( -0.1508021419688953257, 0.4665171419162804645, 0.3606502365330822579 ) ) ;
#16752=DIRECTION ( 'NONE',  ( -7.771561172376107616E-16, 7.170354002788761615E-17, -1.000000000000000000 ) ) ;
#16786=VERTEX_POINT ( 'NONE', #33688 ) ;
#16801=DIRECTION ( 'NONE',  ( 7.771561172376107616E-16, -7.170354002788761615E-17, 1.000000000000000000 ) ) ;
#16813=CARTESIAN_POINT ( 'NONE',  ( -0.1515422989582873303, 0.4690188198402805986, 0.3602693336111430500 ) ) ;
#16821=CARTESIAN_POINT ( 'NONE',  ( -0.1999999999999997891, 0.5182417262804744906, 0.3749999999999995559 ) ) ;
#16835=CARTESIAN_POINT ( 'NONE',  ( -0.2666757540196698084, 0.4921670437878978843, 0.3749999999999990008 ) ) ;
#16863=EDGE_LOOP ( 'NONE', ( #15333, #7462, #35661, #29487 ) ) ;
#16879=FACE_OUTER_BOUND ( 'NONE', #22983, .T. ) ;
#16880=CARTESIAN_POINT ( 'NONE',  ( -0.1212602504878787929, -0.5073146173917494339, 0.1528658435936968152 ) ) ;
#16908=CARTESIAN_POINT ( 'NONE',  ( -0.2300000000000002043, 0.5182417262804744906, 0.08500000000000018652 ) ) ;
#17060=VERTEX_POINT ( 'NONE', #25963 ) ;
#17069=DIRECTION ( 'NONE',  ( 7.771561172376107616E-16, -7.170354002788761615E-17, 1.000000000000000000 ) ) ;
#17102=ADVANCED_FACE ( 'NONE', ( #26347 ), #38269, .T. ) ;
#17150=VERTEX_POINT ( 'NONE', #7009 ) ;
#17156=CARTESIAN_POINT ( 'NONE',  ( -0.1151895542371739328, -0.5267561842548686979, 0.1296992319623857803 ) ) ;
#17270=CARTESIAN_POINT ( 'NONE',  ( -0.1680316146028532909, 0.5219773800263015628, 0.3170215181389818837 ) ) ;
#17271=CARTESIAN_POINT ( 'NONE',  ( -0.1684323897529161340, 0.5231977509870414655, 0.3108929459560476061 ) ) ;
#17321=DIRECTION ( 'NONE',  ( -0.1871397384865028379, -0.9823333030490229989, -6.060229385358974537E-17 ) ) ;
#17339=ORIENTED_EDGE ( 'NONE', *, *, #32105, .T. ) ;
#17387=CIRCLE ( 'NONE', #2276, 0.9237847906030128842 ) ;
#17392=DIRECTION ( 'NONE',  ( 7.771561172376107616E-16, -7.170354002788761615E-17, 1.000000000000000000 ) ) ;
#17416=ORIENTED_EDGE ( 'NONE', *, *, #36565, .T. ) ;
#17419=APPLICATION_CONTEXT ( 'configuration controlled 3d designs of mechanical parts and assemblies' ) ;
#17430=EDGE_CURVE ( 'NONE', #35502, #29923, #31688, .T. ) ;
#17432=DIRECTION ( 'NONE',  ( -1.000000000000000000, 0.000000000000000000, -7.515112548955566195E-16 ) ) ;
#17457=CARTESIAN_POINT ( 'NONE',  ( -0.1613941803225978633, 0.5013693709968672918, 0.1260513636289611328 ) ) ;
#17468=ORIENTED_EDGE ( 'NONE', *, *, #14962, .T. ) ;
#17483=CARTESIAN_POINT ( 'NONE',  ( -0.1126900943766889623, -0.5191528597923187327, 0.1491007326289494894 ) ) ;
#17495=CARTESIAN_POINT ( 'NONE',  ( -0.1196588179077709702, -0.4996288669916955083, 0.3264677846082026380 ) ) ;
#17521=ADVANCED_FACE ( 'NONE', ( #19751 ), #22876, .T. ) ;
#17550=ORIENTED_EDGE ( 'NONE', *, *, #13270, .T. ) ;
#17553=DIRECTION ( 'NONE',  ( 0.000000000000000000, 0.000000000000000000, -1.000000000000000000 ) ) ;
#17574=CARTESIAN_POINT ( 'NONE',  ( -0.1157923916715208196, -0.5295015842444287246, 0.1380392329925462791 ) ) ;
#17577=EDGE_LOOP ( 'NONE', ( #367, #2120, #24203, #18830, #22321, #33287 ) ) ;
#17609=CYLINDRICAL_SURFACE ( 'NONE', #10588, 0.06000000000000021289 ) ;
#17617=CARTESIAN_POINT ( 'NONE',  ( -0.2300000000000000100, 0.5182417262804744906, 0.3749999999999995559 ) ) ;
#17700=CARTESIAN_POINT ( 'NONE',  ( -0.1667650433730277770, 0.4848728453260193749, 0.3315300532330285321 ) ) ;
#17712=CARTESIAN_POINT ( 'NONE',  ( -1.019575837292303166, -0.04310840302197994911, 0.08499999999999990896 ) ) ;
#17731=DIRECTION ( 'NONE',  ( 0.8150167559926634331, 0.5794373887239202547, 1.138269997360109576E-15 ) ) ;
#17744=ORIENTED_EDGE ( 'NONE', *, *, #22058, .F. ) ;
#17808=EDGE_CURVE ( 'NONE', #7716, #34573, #31001, .T. ) ;
#17823=B_SPLINE_CURVE_WITH_KNOTS ( 'NONE', 3,
 ( #23147, #29705, #26425, #29505, #23748, #17156, #14275, #17574 ),
 .UNSPECIFIED., .F., .F.,
 ( 4, 2, 2, 4 ),
 ( 0.0005881714484888313221, 0.001255587419990858997, 0.001589295405741874461, 0.001923003391492890141 ),
 .UNSPECIFIED. ) ;
#17857=ORIENTED_EDGE ( 'NONE', *, *, #297, .T. ) ;
#17866=CARTESIAN_POINT ( 'NONE',  ( -0.1684323895664698867, 0.5231977504175417959, 0.3032895567580831675 ) ) ;
#17903=ORIENTED_EDGE ( 'NONE', *, *, #21244, .T. ) ;
#17945=ORIENTED_EDGE ( 'NONE', *, *, #1372, .F. ) ;
#17948=VERTEX_POINT ( 'NONE', #1560 ) ;
#17959=CIRCLE ( 'NONE', #24560, 0.9237847906030128842 ) ;
#18021=DIRECTION ( 'NONE',  ( 1.000000000000000000, 1.373428330785185865E-31, -7.771561172376106630E-16 ) ) ;
#18030=CARTESIAN_POINT ( 'NONE',  ( -0.1455608194604310901, -0.5249067277714107860, 0.3749999999999998335 ) ) ;
#18034=CIRCLE ( 'NONE', #2279, 1.991674066779348218 ) ;
#18061=CARTESIAN_POINT ( 'NONE',  ( -0.1710642718812839524, 0.4986889572247744096, 0.1528658435937167159 ) ) ;
#18086=EDGE_CURVE ( 'NONE', #35323, #23884, #34974, .T. ) ;
#18182=DIRECTION ( 'NONE',  ( 1.000000000000000000, 1.169383359989551318E-31, -7.771561172376106630E-16 ) ) ;
#18200=EDGE_CURVE ( 'NONE', #32882, #34195, #19375, .T. ) ;
#18219=DIRECTION ( 'NONE',  ( -0.4887635750373022780, -0.8724162812079766516, -1.864855553833737887E-16 ) ) ;
#18221=CARTESIAN_POINT ( 'NONE',  ( -0.1157923916715208196, -0.5295015842444287246, 0.1380392329925462791 ) ) ;
#18233=ORIENTED_EDGE ( 'NONE', *, *, #9756, .F. ) ;
#18239=AXIS2_PLACEMENT_3D ( 'NONE', #16908, #34655, #22328 ) ;
#18290=CARTESIAN_POINT ( 'NONE',  ( -0.1212602504878778492, -0.5073146173917499890, 0.3048175120576743780 ) ) ;
#18330=DIRECTION ( 'NONE',  ( -7.771561172376107616E-16, 7.170354002788761615E-17, -1.000000000000000000 ) ) ;
#18344=PRODUCT_CONTEXT ( 'NONE', #35544, 'mechanical' ) ;
#18369=DIRECTION ( 'NONE',  ( -7.771561172376107616E-16, 7.170354002788761615E-17, -1.000000000000000000 ) ) ;
#18436=CARTESIAN_POINT ( 'NONE',  ( -0.06919656468380842862, -0.09959325338431362917, 0.09813923389047245205 ) ) ;
#18455=CARTESIAN_POINT ( 'NONE',  ( -0.1684323896977243107, 0.5231977508184618708, 0.1451849067762387424 ) ) ;
#18502=ORIENTED_EDGE ( 'NONE', *, *, #20480, .F. ) ;
#18519=CARTESIAN_POINT ( 'NONE',  ( -0.1212602504510638252, -0.5073146174426025334, 0.3063129689661515664 ) ) ;
#18531=CARTESIAN_POINT ( 'NONE',  ( -0.1138236225804901969, -0.5205343845807010039, 0.3387850541077452871 ) ) ;
#18565=EDGE_LOOP ( 'NONE', ( #35117, #6649, #27061, #17945, #18502 ) ) ;
#18672=AXIS2_PLACEMENT_3D ( 'NONE', #5036, #17392, #20697 ) ;
#18691=CARTESIAN_POINT ( 'NONE',  ( -0.2600000000000004530, 0.5182417262804744906, 0.08500000000000017264 ) ) ;
#18702=AXIS2_PLACEMENT_3D ( 'NONE', #37159, #24825, #18021 ) ;
#18715=ORIENTED_EDGE ( 'NONE', *, *, #24992, .F. ) ;
#18744=CIRCLE ( 'NONE', #26620, 1.986674066779348102 ) ;
#18766=CIRCLE ( 'NONE', #4941, 0.06000000000000031697 ) ;
#18781=ORIENTED_EDGE ( 'NONE', *, *, #6808, .F. ) ;
#18808=EDGE_CURVE ( 'NONE', #3414, #29923, #27142, .T. ) ;
#18830=ORIENTED_EDGE ( 'NONE', *, *, #30543, .F. ) ;
#18878=B_SPLINE_CURVE_WITH_KNOTS ( 'NONE', 3,
 ( #40543, #15244, #18531, #40336, #12165, #24728, #15653, #28617 ),
 .UNSPECIFIED., .F., .F.,
 ( 4, 2, 2, 4 ),
 ( -9.185902906383436317E-17, 0.0008552058350302804311, 0.001282808752545464394, 0.001710411670060648683 ),
 .UNSPECIFIED. ) ;
#19001=DIRECTION ( 'NONE',  ( 1.000000000000000000, 0.000000000000000000, 8.537024980200792236E-16 ) ) ;
#19008=CYLINDRICAL_SURFACE ( 'NONE', #13580, 0.03000000000000022787 ) ;
#19024=FACE_OUTER_BOUND ( 'NONE', #23897, .T. ) ;
#19030=EDGE_LOOP ( 'NONE', ( #17903, #8482, #4713, #17744 ) ) ;
#19133=VERTEX_POINT ( 'NONE', #4602 ) ;
#19203=CARTESIAN_POINT ( 'NONE',  ( -0.2043922129835731294, -0.5166151207188712791, 0.3750000000000001110 ) ) ;
#19208=DIRECTION ( 'NONE',  ( -3.406373435249024214E-19, -1.000000000000000000, -7.170354002788761615E-17 ) ) ;
#19225=( BOUNDED_SURFACE ( )  B_SPLINE_SURFACE ( 3, 2, ( 
 ( #1160, #12868, #34859 ),
 ( #6668, #4198, #19244 ),
 ( #31787, #13471, #3601 ),
 ( #10182, #16169, #26038 ),
 ( #28706, #25617, #9972 ),
 ( #31988, #3800, #16356 ),
 ( #28891, #22751, #35278 ),
 ( #38560, #7073, #19644 ) ),
 .UNSPECIFIED., .F., .F., .T. ) 
 B_SPLINE_SURFACE_WITH_KNOTS ( ( 4, 2, 2, 4 ),
 ( 3, 3 ),
 ( 0.001363486440777415343, 0.002314916752335400337, 0.002790631908114392726, 0.003266347063893385548 ),
 ( 0.000000000000000000, 1.000000000000000000 ),
 .UNSPECIFIED. ) 
 GEOMETRIC_REPRESENTATION_ITEM ( )  RATIONAL_B_SPLINE_SURFACE ( (
 ( 1.000000000000000000, 0.9128709291752513666, 1.000000000000000000),
 ( 1.000000000000000000, 0.9128773865067255633, 1.000000000000000000),
 ( 1.000000000000000000, 0.9126892044530536818, 1.000000000000000000),
 ( 1.000000000000000000, 0.9123262075125851966, 1.000000000000000000),
 ( 1.000000000000000000, 0.9121926916485024739, 1.000000000000000000),
 ( 1.000000000000000000, 0.9119580040447240465, 1.000000000000000000),
 ( 1.000000000000000000, 0.9118544196722184747, 1.000000000000000000),
 ( 1.000000000000000000, 0.9117915798251763349, 1.000000000000000000) ) ) 
 REPRESENTATION_ITEM ( '' )  SURFACE ( )  );
#19244=CARTESIAN_POINT ( 'NONE',  ( -0.1157351144567332346, -0.4800210170677816079, 0.3382895569177964967 ) ) ;
#19297=ORIENTED_EDGE ( 'NONE', *, *, #20480, .T. ) ;
#19314=EDGE_CURVE ( 'NONE', #9065, #9709, #35063, .T. ) ;
#19366=VECTOR ( 'NONE', #24687, 39.37007874015748143 ) ;
#19375=LINE ( 'NONE', #680, #24467 ) ;
#19392=ORIENTED_EDGE ( 'NONE', *, *, #28978, .T. ) ;
#19402=CARTESIAN_POINT ( 'NONE',  ( -2.070754768975505034, -0.09959325338431362917, 0.3602693341844379060 ) ) ;
#19480=EDGE_CURVE ( 'NONE', #9996, #35502, #35023, .T. ) ;
#19487=FACE_OUTER_BOUND ( 'NONE', #7206, .T. ) ;
#19537=ORIENTED_EDGE ( 'NONE', *, *, #22315, .F. ) ;
#19558=ORIENTED_EDGE ( 'NONE', *, *, #11756, .F. ) ;
#19567=CARTESIAN_POINT ( 'NONE',  ( -0.1552056223146390523, 0.4812861443614941392, 0.3591723288241918666 ) ) ;
#19583=CYLINDRICAL_SURFACE ( 'NONE', #23038, 0.03000000000000022787 ) ;
#19586=DIRECTION ( 'NONE',  ( 0.000000000000000000, 0.000000000000000000, -1.000000000000000000 ) ) ;
#19644=CARTESIAN_POINT ( 'NONE',  ( -0.1210148435730238475, -0.5061394519557863569, 0.3122829191279349881 ) ) ;
#19646=ORIENTED_EDGE ( 'NONE', *, *, #40100, .T. ) ;
#19652=DIRECTION ( 'NONE',  ( -1.000000000000000000, 0.000000000000000000, -5.691349986800505477E-16 ) ) ;
#19662=EDGE_LOOP ( 'NONE', ( #16149, #18715, #19558, #8418, #12974 ) ) ;
#19696=EDGE_CURVE ( 'NONE', #10838, #16489, #17959, .T. ) ;
#19721=DIRECTION ( 'NONE',  ( -0.2147743920926257211, -0.9766636885342073748, -1.901964324923283986E-17 ) ) ;
#19751=FACE_OUTER_BOUND ( 'NONE', #39751, .T. ) ;
#19754=CIRCLE ( 'NONE', #12529, 0.06000000000000021289 ) ;
#19876=DIRECTION ( 'NONE',  ( 1.000000000000000000, 0.000000000000000000, 7.515112548955565209E-16 ) ) ;
#19884=ORIENTED_EDGE ( 'NONE', *, *, #23552, .F. ) ;
#19957=CARTESIAN_POINT ( 'NONE',  ( -0.1628177922134119437, 0.5059000297268509971, 0.3228062255482125331 ) ) ;
#19963=CIRCLE ( 'NONE', #25216, 0.02999999999999998848 ) ;
#19982=ADVANCED_FACE ( 'NONE', ( #14544 ), #27111, .T. ) ;
#20001=CIRCLE ( 'NONE', #2270, 0.01499999999999997689 ) ;
#20003=CIRCLE ( 'NONE', #20654, 1.991674066779348218 ) ;
#20046=DIRECTION ( 'NONE',  ( -7.771561172376107616E-16, 7.170354002788761615E-17, -1.000000000000000000 ) ) ;
#20087=EDGE_CURVE ( 'NONE', #9596, #23678, #21269, .T. ) ;
#20105=CARTESIAN_POINT ( 'NONE',  ( -0.1508044614562676355, 0.4665164580004940720, 0.3602693336111434941 ) ) ;
#20142=CARTESIAN_POINT ( 'NONE',  ( -0.1157923916715208196, -0.5295015842444287246, 0.3599999999999993205 ) ) ;
#20148=CARTESIAN_POINT ( 'NONE',  ( -0.1157923916715205420, -0.5295015842444287246, 0.09999999999999989453 ) ) ;
#20156=ORIENTED_EDGE ( 'NONE', *, *, #30297, .F. ) ;
#20165=ORIENTED_EDGE ( 'NONE', *, *, #4920, .T. ) ;
#20173=CARTESIAN_POINT ( 'NONE',  ( -0.1613545236348712109, 0.5011730501305514673, 0.3493272269784499229 ) ) ;
#20177=DIRECTION ( 'NONE',  ( 7.771561172376107616E-16, -7.170354002788761615E-17, 1.000000000000000000 ) ) ;
#20230=EDGE_CURVE ( 'NONE', #38543, #39260, #8803, .T. ) ;
#20269=CARTESIAN_POINT ( 'NONE',  ( -0.08408070219615630669, -0.09959325338431362917, 0.3749999999999960587 ) ) ;
#20271=CARTESIAN_POINT ( 'NONE',  ( -0.1999999999999999833, 0.5182417262804744906, 0.08500000000000017264 ) ) ;
#20292=CARTESIAN_POINT ( 'NONE',  ( -1.019575837292303166, -0.04310840302197994911, 0.3599999999999993205 ) ) ;
#20346=B_SPLINE_CURVE_WITH_KNOTS ( 'NONE', 3,
 ( #39437, #36351, #7764, #4870 ),
 .UNSPECIFIED., .F., .F.,
 ( 4, 4 ),
 ( -2.702335329567562820E-05, 0.0001957598036966991110 ),
 .UNSPECIFIED. ) ;
#20348=CARTESIAN_POINT ( 'NONE',  ( -0.1588702854552149490, 0.4932535771925480872, 0.1179163363090275640 ) ) ;
#20359=ORIENTED_EDGE ( 'NONE', *, *, #14752, .T. ) ;
#20366=CARTESIAN_POINT ( 'NONE',  ( -0.1653405084325548779, 0.5136906775330246644, 0.3358539725464951275 ) ) ;
#20368=DIRECTION ( 'NONE',  ( -7.771561172376107616E-16, 7.170354002788761615E-17, -1.000000000000000000 ) ) ;
#20380=CIRCLE ( 'NONE', #10585, 0.02999999999999998154 ) ;
#20468=AXIS2_PLACEMENT_3D ( 'NONE', #640, #12736, #6751 ) ;
#20480=EDGE_CURVE ( 'NONE', #8954, #16786, #22827, .T. ) ;
#20508=FACE_OUTER_BOUND ( 'NONE', #8134, .T. ) ;
#20538=EDGE_LOOP ( 'NONE', ( #7350, #21711, #35175, #22484 ) ) ;
#20539=EDGE_CURVE ( 'NONE', #4767, #40606, #21297, .T. ) ;
#20594=CARTESIAN_POINT ( 'NONE',  ( -0.1509132741912886377, 0.4664843738648666305, 0.09813923389061204872 ) ) ;
#20654=AXIS2_PLACEMENT_3D ( 'NONE', #29137, #25249, #9803 ) ;
#20677=VECTOR ( 'NONE', #5193, 39.37007874015748143 ) ;
#20697=DIRECTION ( 'NONE',  ( 1.000000000000000000, 0.000000000000000000, 0.000000000000000000 ) ) ;
#20700=DIRECTION ( 'NONE',  ( -6.217248937900885304E-15, 2.158931604386568927E-14, 1.000000000000000000 ) ) ;
#20702=DIRECTION ( 'NONE',  ( -7.771561172376107616E-16, 7.170354002788761615E-17, -1.000000000000000000 ) ) ;
#20703=DIRECTION ( 'NONE',  ( 7.771561172376107616E-16, -7.170354002788761615E-17, 1.000000000000000000 ) ) ;
#20706=CARTESIAN_POINT ( 'NONE',  ( -0.1574377185082707353, 0.4885537809602777948, 0.09999999999999989453 ) ) ;
#20727=ADVANCED_FACE ( 'NONE', ( #8384 ), #11658, .T. ) ;
#20760=CARTESIAN_POINT ( 'NONE',  ( -0.1688425296110669938, 0.4915895952456239004, 0.1316117873487830936 ) ) ;
#20787=CARTESIAN_POINT ( 'NONE',  ( -0.2299999999999999267, 0.5182417262804744906, 0.3599999999999993205 ) ) ;
#20811=ORIENTED_EDGE ( 'NONE', *, *, #628, .F. ) ;
#20884=FACE_OUTER_BOUND ( 'NONE', #24843, .T. ) ;
#20895=ORIENTED_EDGE ( 'NONE', *, *, #40100, .F. ) ;
#20952=CARTESIAN_POINT ( 'NONE',  ( -0.1699617389507570020, 0.4951775333576697302, 0.1374137075621912063 ) ) ;
#20958=CARTESIAN_POINT ( 'NONE',  ( -2.070754768975505034, -0.09959325338431362917, 0.3749999999999976130 ) ) ;
#20976=FACE_OUTER_BOUND ( 'NONE', #39161, .T. ) ;
#20999=EDGE_CURVE ( 'NONE', #11394, #8287, #33114, .T. ) ;
#21002=EDGE_CURVE ( 'NONE', #12958, #16211, #20003, .T. ) ;
#21050=DIRECTION ( 'NONE',  ( 0.9766636885342061536, -0.2147743920926307448, 0.000000000000000000 ) ) ;
#21091=LINE ( 'NONE', #39803, #22631 ) ;
#21105=ADVANCED_FACE ( 'NONE', ( #26872 ), #7522, .T. ) ;
#21158=ORIENTED_EDGE ( 'NONE', *, *, #25816, .T. ) ;
#21173=CARTESIAN_POINT ( 'NONE',  ( -0.1642263571684414447, 0.5103503754387010982, 0.3032895567580821683 ) ) ;
#21190=VERTEX_POINT ( 'NONE', #20706 ) ;
#21191=CARTESIAN_POINT ( 'NONE',  ( -0.1127285386968538555, -0.5155187098904498999, 0.1369073159184197586 ) ) ;
#21199=CYLINDRICAL_SURFACE ( 'NONE', #21865, 0.06000000000000031697 ) ;
#21244=EDGE_CURVE ( 'NONE', #1527, #17060, #6186, .T. ) ;
#21264=CYLINDRICAL_SURFACE ( 'NONE', #25730, 2.001674066779348227 ) ;
#21269=CIRCLE ( 'NONE', #3524, 0.01500000000000001159 ) ;
#21278=CIRCLE ( 'NONE', #29816, 1.986674066779348102 ) ;
#21282=( LENGTH_UNIT ( ) NAMED_UNIT ( * ) SI_UNIT ( $, .METRE. ) );
#21290=CIRCLE ( 'NONE', #29830, 2.001671648589471442 ) ;
#21297=CIRCLE ( 'NONE', #34410, 1.986674066779348102 ) ;
#21331=DIRECTION ( 'NONE',  ( 1.000000000000000000, 3.035386659626938621E-15, 7.588466649067346553E-16 ) ) ;
#21372=CARTESIAN_POINT ( 'NONE',  ( -0.1707856549140114588, 0.4978063840003627005, 0.1437995925080555182 ) ) ;
#21423=ORIENTED_EDGE ( 'NONE', *, *, #36612, .F. ) ;
#21436=CARTESIAN_POINT ( 'NONE',  ( -0.1339136704200478145, -0.4685718226220191851, 0.09550516381870249871 ) ) ;
#21468=EDGE_LOOP ( 'NONE', ( #34519, #14466, #39999, #1683 ) ) ;
#21497=B_SPLINE_CURVE_WITH_KNOTS ( 'NONE', 3,
 ( #31337, #37281, #36874, #5803 ),
 .UNSPECIFIED., .F., .F.,
 ( 4, 4 ),
 ( -1.150894640811756038E-05, 0.0005747792170237749076 ),
 .UNSPECIFIED. ) ;
#21526=FACE_OUTER_BOUND ( 'NONE', #29842, .T. ) ;
#21527=ORIENTED_EDGE ( 'NONE', *, *, #32105, .F. ) ;
#21537=ORIENTED_EDGE ( 'NONE', *, *, #4170, .T. ) ;
#21600=EDGE_CURVE ( 'NONE', #9596, #30066, #38397, .T. ) ;
#21607=CARTESIAN_POINT ( 'NONE',  ( -0.2136509456379319383, -0.4946207598421926699, 0.09999999999999989453 ) ) ;
#21608=CARTESIAN_POINT ( 'NONE',  ( -0.1212602504878774051, -0.5073146173917496560, 0.1528658435937000626 ) ) ;
#21611=CARTESIAN_POINT ( 'NONE',  ( -0.1154362047090707333, -0.5278818619434392234, 0.1319635891399765504 ) ) ;
#21661=ORIENTED_EDGE ( 'NONE', *, *, #1902, .F. ) ;
#21695=VERTEX_POINT ( 'NONE', #13573 ) ;
#21711=ORIENTED_EDGE ( 'NONE', *, *, #19696, .F. ) ;
#21726=AXIS2_PLACEMENT_3D ( 'NONE', #9957, #28088, #31376 ) ;
#21758=AXIS2_PLACEMENT_3D ( 'NONE', #31235, #36979, #8799 ) ;
#21784=CARTESIAN_POINT ( 'NONE',  ( -0.1210148435730253880, -0.5061394519557965710, 0.3122829191278980177 ) ) ;
#21827=FACE_OUTER_BOUND ( 'NONE', #10504, .T. ) ;
#21829=ORIENTED_EDGE ( 'NONE', *, *, #8061, .F. ) ;
#21865=AXIS2_PLACEMENT_3D ( 'NONE', #24294, #15026, #27394 ) ;
#21878=VERTEX_POINT ( 'NONE', #8805 ) ;
#21894=SHAPE_REPRESENTATION_RELATIONSHIP ( 'NONE' , 'NONE' ,  #40103, #5887 ) ;
#21944=FACE_BOUND ( 'NONE', #33927, .T. ) ;
#22000=EDGE_CURVE ( 'NONE', #26316, #1752, #35504, .T. ) ;
#22026=ORIENTED_EDGE ( 'NONE', *, *, #27106, .T. ) ;
#22043=CARTESIAN_POINT ( 'NONE',  ( -0.1212602504878781962, -0.5073146173917492119, 0.3032895567580783380 ) ) ;
#22058=EDGE_CURVE ( 'NONE', #1527, #26316, #13878, .T. ) ;
#22136=ADVANCED_FACE ( 'NONE', ( #20884 ), #2191, .T. ) ;
#22271=ORIENTED_EDGE ( 'NONE', *, *, #36823, .T. ) ;
#22297=ORIENTED_EDGE ( 'NONE', *, *, #24100, .F. ) ;
#22311=VERTEX_POINT ( 'NONE', #15501 ) ;
#22315=EDGE_CURVE ( 'NONE', #39656, #4670, #27245, .T. ) ;
#22321=ORIENTED_EDGE ( 'NONE', *, *, #38776, .F. ) ;
#22328=DIRECTION ( 'NONE',  ( -1.000000000000000000, 0.000000000000000000, -5.691349986800505477E-16 ) ) ;
#22345=ADVANCED_FACE ( 'NONE', ( #2950 ), #22424, .T. ) ;
#22424=TOROIDAL_SURFACE ( 'NONE', #32229, 1.971674066779348866, 0.02999999999999999889 ) ;
#22427=DIRECTION ( 'NONE',  ( 1.000000000000000000, 0.000000000000000000, 7.906745362128971688E-16 ) ) ;
#22440=ORIENTED_EDGE ( 'NONE', *, *, #17430, .F. ) ;
#22479=ORIENTED_EDGE ( 'NONE', *, *, #29933, .F. ) ;
#22484=ORIENTED_EDGE ( 'NONE', *, *, #24547, .F. ) ;
#22500=CARTESIAN_POINT ( 'NONE',  ( -0.1443922129835726875, -0.5166151207188712791, 0.3750000000000001110 ) ) ;
#22521=ORIENTED_EDGE ( 'NONE', *, *, #13909, .T. ) ;
#22605=DIRECTION ( 'NONE',  ( 7.771561172376107616E-16, -7.170354002788761615E-17, 1.000000000000000000 ) ) ;
#22631=VECTOR ( 'NONE', #5231, 39.37007874015748143 ) ;
#22639=DIRECTION ( 'NONE',  ( 7.771561172376107616E-16, -7.170354002788761615E-17, 1.000000000000000000 ) ) ;
#22654=CARTESIAN_POINT ( 'NONE',  ( -0.1710642718812833418, 0.4986889572247755753, 0.1528658435937000626 ) ) ;
#22694=ORIENTED_EDGE ( 'NONE', *, *, #21600, .F. ) ;
#22751=CARTESIAN_POINT ( 'NONE',  ( -0.1127323924368017344, -0.5155369761421052521, 0.3191796960528185401 ) ) ;
#22817=CARTESIAN_POINT ( 'NONE',  ( -2.070754768975505034, -0.09959325338431362917, 0.09999999999999933942 ) ) ;
#22827=B_SPLINE_CURVE_WITH_KNOTS ( 'NONE', 3,
 ( #249, #9663, #29193, #13351 ),
 .UNSPECIFIED., .F., .F.,
 ( 4, 4 ),
 ( 1.873907885762902204E-16, 0.0005779611142783052345 ),
 .UNSPECIFIED. ) ;
#22874=CARTESIAN_POINT ( 'NONE',  ( -0.1646293987946891302, 0.5114631127588012971, 0.3384789781300878708 ) ) ;
#22876=CYLINDRICAL_SURFACE ( 'NONE', #12613, 0.02999999999999998848 ) ;
#22907=ORIENTED_EDGE ( 'NONE', *, *, #18808, .T. ) ;
#22979=FACE_OUTER_BOUND ( 'NONE', #21468, .T. ) ;
#22983=EDGE_LOOP ( 'NONE', ( #37589, #28678, #6595, #37205, #36007, #6450 ) ) ;
#22987=DIRECTION ( 'NONE',  ( 7.771561172376107616E-16, -7.170354002788761615E-17, 1.000000000000000000 ) ) ;
#23038=AXIS2_PLACEMENT_3D ( 'NONE', #25970, #509, #32118 ) ;
#23064=AXIS2_PLACEMENT_3D ( 'NONE', #31875, #19721, #16431 ) ;
#23075=ORIENTED_EDGE ( 'NONE', *, *, #7909, .T. ) ;
#23112=( NAMED_UNIT ( * ) SI_UNIT ( $, .STERADIAN. ) SOLID_ANGLE_UNIT ( ) );
#23131=EDGE_CURVE ( 'NONE', #38042, #40606, #34227, .T. ) ;
#23147=CARTESIAN_POINT ( 'NONE',  ( -0.1088121136105147380, -0.4964308608213456875, 0.09999999999999989453 ) ) ;
#23150=EDGE_LOOP ( 'NONE', ( #20811, #25856 ) ) ;
#23151=AXIS2_PLACEMENT_3D ( 'NONE', #22817, #9633, #16405 ) ;
#23165=DIRECTION ( 'NONE',  ( 1.498801083243964091E-15, 2.706744618697167655E-15, 1.000000000000000000 ) ) ;
#23216=CARTESIAN_POINT ( 'NONE',  ( -0.08408070219615712548, -0.09959325338431362917, 0.1000000000000008799 ) ) ;
#23232=ORIENTED_EDGE ( 'NONE', *, *, #17430, .T. ) ;
#23242=DIRECTION ( 'NONE',  ( 7.771561172376107616E-16, -7.170354002788761615E-17, 1.000000000000000000 ) ) ;
#23247=AXIS2_PLACEMENT_3D ( 'NONE', #39643, #3035, #25452 ) ;
#23257=CARTESIAN_POINT ( 'NONE',  ( -0.1157923916715208196, -0.5295015842444287246, 0.3181161673586317962 ) ) ;
#23263=CARTESIAN_POINT ( 'NONE',  ( -0.1574156176409247099, 0.4885425907994572214, 0.3417174393643599428 ) ) ;
#23279=DIRECTION ( 'NONE',  ( -7.771561172376107616E-16, 7.170354002788761615E-17, -1.000000000000000000 ) ) ;
#23366=ADVANCED_FACE ( 'NONE', ( #34888 ), #13237, .T. ) ;
#23398=DIMENSIONAL_EXPONENTS ( 1.000000000000000000, 0.000000000000000000, 0.000000000000000000, 0.000000000000000000, 0.000000000000000000, 0.000000000000000000, 0.000000000000000000 ) ;
#23419=CARTESIAN_POINT ( 'NONE',  ( -0.1167294259372883281, -0.5331983348239501819, 0.3032895567580801144 ) ) ;
#23476=CARTESIAN_POINT ( 'NONE',  ( -0.1710642717598274409, 0.4986889574319069429, 0.3078512670230414972 ) ) ;
#23501=EDGE_LOOP ( 'NONE', ( #11895, #9014, #36273, #36065 ) ) ;
#23552=EDGE_CURVE ( 'NONE', #16489, #15152, #6004, .T. ) ;
#23553=CARTESIAN_POINT ( 'NONE',  ( -0.1710642718812828145, 0.4986889572247755198, 0.3749999999999990008 ) ) ;
#23588=CARTESIAN_POINT ( 'NONE',  ( -0.1969433606228600808, 0.5138636982738217229, 0.1528658435937000626 ) ) ;
#23596=DIRECTION ( 'NONE',  ( 7.771561172376107616E-16, -7.170354002788761615E-17, 1.000000000000000000 ) ) ;
#23607=FACE_OUTER_BOUND ( 'NONE', #20538, .T. ) ;
#23643=CARTESIAN_POINT ( 'NONE',  ( -0.1673869564144402633, 0.4868872877193594073, 0.1265580611896349461 ) ) ;
#23662=CARTESIAN_POINT ( 'NONE',  ( -0.1211791774340214151, -0.5069275750892356935, 0.1468366819525818712 ) ) ;
#23669=PRODUCT_DEFINITION_CONTEXT ( 'detailed design', #17419, 'design' ) ;
#23678=VERTEX_POINT ( 'NONE', #37463 ) ;
#23693=CARTESIAN_POINT ( 'NONE',  ( -0.1603938765018562418, 0.4636889572247986369, 0.3382895567582878127 ) ) ;
#23740=CARTESIAN_POINT ( 'NONE',  ( -2.070754768975505034, -0.09959325338431362917, 0.3749999999999976130 ) ) ;
#23748=CARTESIAN_POINT ( 'NONE',  ( -0.1142976700078418423, -0.5226524673290435796, 0.1219895833617483799 ) ) ;
#23758=B_SPLINE_CURVE_WITH_KNOTS ( 'NONE', 3,
 ( #21784, #33933, #5732, #18290, #30830 ),
 .UNSPECIFIED., .F., .F.,
 ( 4, 1, 4 ),
 ( 0.003975523017580754465, 0.004090739973965718326, 0.004205956930350682188 ),
 .UNSPECIFIED. ) ;
#23792=ORIENTED_EDGE ( 'NONE', *, *, #9532, .T. ) ;
#23800=AXIS2_PLACEMENT_3D ( 'NONE', #28817, #7002, #7602 ) ;
#23841=CARTESIAN_POINT ( 'NONE',  ( -0.1684323895664520399, 0.5231977504174887272, 0.3032895567580809471 ) ) ;
#23869=CARTESIAN_POINT ( 'NONE',  ( -0.1163549140004290217, -0.5320595946631634376, 0.1429098354138644833 ) ) ;
#23884=VERTEX_POINT ( 'NONE', #10503 ) ;
#23897=EDGE_LOOP ( 'NONE', ( #29745, #14201, #17339, #33124 ) ) ;
#23995=ORIENTED_EDGE ( 'NONE', *, *, #22058, .T. ) ;
#24039=ADVANCED_FACE ( 'NONE', ( #3087 ), #34823, .T. ) ;
#24050=( BOUNDED_SURFACE ( )  B_SPLINE_SURFACE ( 3, 2, ( 
 ( #28408, #38671, #13772 ),
 ( #23662, #11301, #23869 ),
 ( #36186, #17483, #11104 ),
 ( #16880, #10695, #29421 ) ),
 .UNSPECIFIED., .F., .F., .T. ) 
 B_SPLINE_SURFACE_WITH_KNOTS ( ( 4, 4 ),
 ( 3, 3 ),
 ( 0.0007843053012490898077, 0.001168341556843950548 ),
 ( 0.000000000000000000, 1.000000000000000000 ),
 .UNSPECIFIED. ) 
 GEOMETRIC_REPRESENTATION_ITEM ( )  RATIONAL_B_SPLINE_SURFACE ( (
 ( 1.000000000000000000, 0.9117915798263362959, 1.000000000000000000),
 ( 1.000000000000000000, 0.9032018617293641194, 1.000000000000000000),
 ( 1.000000000000000000, 0.8990088477696668301, 1.000000000000000000),
 ( 1.000000000000000000, 0.8989970956543188452, 1.000000000000000000) ) ) 
 REPRESENTATION_ITEM ( '' )  SURFACE ( )  );
#24055=CARTESIAN_POINT ( 'NONE',  ( -0.1665325656947614918, 0.5173663872579224998, 0.1272034666820887894 ) ) ;
#24066=DIRECTION ( 'NONE',  ( -7.771561172376107616E-16, 7.170354002788761615E-17, -1.000000000000000000 ) ) ;
#24083=CARTESIAN_POINT ( 'NONE',  ( -0.2900000000000003131, 0.5182417262804744906, 0.3749999999999995004 ) ) ;
#24100=EDGE_CURVE ( 'NONE', #35807, #11394, #24484, .T. ) ;
#24121=DIRECTION ( 'NONE',  ( -7.771561172376107616E-16, 7.170354002788761615E-17, -1.000000000000000000 ) ) ;
#24161=FACE_OUTER_BOUND ( 'NONE', #2030, .T. ) ;
#24197=CARTESIAN_POINT ( 'NONE',  ( -0.1969433606228599420, 0.5138636982738220560, 0.3032895567580801144 ) ) ;
#24203=ORIENTED_EDGE ( 'NONE', *, *, #20539, .F. ) ;
#24253=FACE_OUTER_BOUND ( 'NONE', #16863, .T. ) ;
#24294=CARTESIAN_POINT ( 'NONE',  ( -0.2300000000000000100, 0.5182417262804744906, 0.3749999999999995559 ) ) ;
#24302=ORIENTED_EDGE ( 'NONE', *, *, #36897, .T. ) ;
#24348=CIRCLE ( 'NONE', #33512, 0.01500000000000001159 ) ;
#24397=CARTESIAN_POINT ( 'NONE',  ( -0.1163200376094536276, -0.5319009979872306726, 0.1426078552794942667 ) ) ;
#24415=PLANE ( 'NONE',  #37615 ) ;
#24447=FACE_BOUND ( 'NONE', #3064, .T. ) ;
#24467=VECTOR ( 'NONE', #16282, 39.37007874015748143 ) ;
#24484=LINE ( 'NONE', #30849, #6579 ) ;
#24494=CARTESIAN_POINT ( 'NONE',  ( -0.1731185243557763487, 0.5373335498847187086, 0.09999999999999989453 ) ) ;
#24512=AXIS2_PLACEMENT_3D ( 'NONE', #32143, #17321, #35630 ) ;
#24534=CARTESIAN_POINT ( 'NONE',  ( -2.070754768975504589, -0.09959325338431362917, 0.3599999999999976552 ) ) ;
#24547=EDGE_CURVE ( 'NONE', #27939, #32882, #27630, .T. ) ;
#24558=AXIS2_PLACEMENT_3D ( 'NONE', #32156, #35651, #32564 ) ;
#24560=AXIS2_PLACEMENT_3D ( 'NONE', #29785, #1627, #1045 ) ;
#24613=CARTESIAN_POINT ( 'NONE',  ( -0.1206014988277951117, -0.5041571071311164998, 0.1364167062886335602 ) ) ;
#24687=DIRECTION ( 'NONE',  ( -7.771561172376107616E-16, 7.170354002788761615E-17, -1.000000000000000000 ) ) ;
#24699=CARTESIAN_POINT ( 'NONE',  ( -0.1111952754772590757, -0.5081759048641385501, 0.1244868412816175218 ) ) ;
#24728=CARTESIAN_POINT ( 'NONE',  ( -0.1082158540381399775, -0.4935046016075750885, 0.3575786101922723281 ) ) ;
#24734=AXIS2_PLACEMENT_3D ( 'NONE', #15177, #24066, #36986 ) ;
#24763=AXIS2_PLACEMENT_3D ( 'NONE', #8716, #14483, #36514 ) ;
#24781=ADVANCED_FACE ( 'NONE', ( #19024 ), #15819, .T. ) ;
#24796=CARTESIAN_POINT ( 'NONE',  ( -2.070754768975505034, -0.09959325338431362917, 0.08499999999999909017 ) ) ;
#24825=DIRECTION ( 'NONE',  ( 7.771561172376107616E-16, -7.170354002788761615E-17, 1.000000000000000000 ) ) ;
#24843=EDGE_LOOP ( 'NONE', ( #1183, #8786, #5949, #32819, #25620 ) ) ;
#24898=CARTESIAN_POINT ( 'NONE',  ( -0.1129900121204040209, -0.5167580615069109484, 0.1415474730881046972 ) ) ;
#24992=EDGE_CURVE ( 'NONE', #35807, #17948, #19754, .T. ) ;
#25030=ADVANCED_FACE ( 'NONE', ( #27439 ), #35508, .T. ) ;
#25031=CARTESIAN_POINT ( 'NONE',  ( -0.1450923023275428325, -0.5230583524816332375, 0.3181161673586312411 ) ) ;
#25196=CARTESIAN_POINT ( 'NONE',  ( -0.1533385355407297923, 0.4750492940987078860, 0.3599999999999995981 ) ) ;
#25210=CARTESIAN_POINT ( 'NONE',  ( -0.1142670043590670731, -0.4723146173917492918, 0.1178658435937000315 ) ) ;
#25216=AXIS2_PLACEMENT_3D ( 'NONE', #24197, #20703, #26680 ) ;
#25249=DIRECTION ( 'NONE',  ( 7.771561172376107616E-16, -7.170354002788761615E-17, 1.000000000000000000 ) ) ;
#25294=VECTOR ( 'NONE', #34322, 39.37007874015748143 ) ;
#25328=CIRCLE ( 'NONE', #6612, 0.01500000000000000118 ) ;
#25336=EDGE_CURVE ( 'NONE', #40606, #23678, #13226, .T. ) ;
#25398=FACE_OUTER_BOUND ( 'NONE', #40561, .T. ) ;
#25452=DIRECTION ( 'NONE',  ( -1.000000000000000000, 0.000000000000000000, -7.847494366974319310E-16 ) ) ;
#25523=CARTESIAN_POINT ( 'NONE',  ( -0.1126900943355985951, -0.5191528601549348920, 0.3070571034469349869 ) ) ;
#25526=ADVANCED_FACE ( 'NONE', ( #30813, #24447, #2634 ), #37579, .T. ) ;
#25561=CARTESIAN_POINT ( 'NONE',  ( -0.1603938765018537715, 0.4636889572247753222, 0.1178658435936994903 ) ) ;
#25585=DIRECTION ( 'NONE',  ( -7.771561172376107616E-16, 7.170354002788761615E-17, -1.000000000000000000 ) ) ;
#25617=CARTESIAN_POINT ( 'NONE',  ( -0.1112012347075035518, -0.5082045352552144735, 0.3316257441459521949 ) ) ;
#25620=ORIENTED_EDGE ( 'NONE', *, *, #4920, .F. ) ;
#25654=EDGE_CURVE ( 'NONE', #21190, #16265, #1422, .T. ) ;
#25655=DIRECTION ( 'NONE',  ( 7.771561172376107616E-16, -7.170354002788761615E-17, 1.000000000000000000 ) ) ;
#25681=CARTESIAN_POINT ( 'NONE',  ( -0.1212602504878774051, -0.5073146173917496560, 0.1528658435937000626 ) ) ;
#25718=AXIS2_PLACEMENT_3D ( 'NONE', #16602, #22987, #32641 ) ;
#25730=AXIS2_PLACEMENT_3D ( 'NONE', #23740, #5393, #8083 ) ;
#25769=CARTESIAN_POINT ( 'NONE',  ( -0.1710642718812833418, 0.4986889572247755753, 0.1528658435937000626 ) ) ;
#25781=CARTESIAN_POINT ( 'NONE',  ( -0.1589779575897101449, 0.4935643744415435519, 0.1021333108076154655 ) ) ;
#25816=EDGE_CURVE ( 'NONE', #21695, #30066, #31976, .T. ) ;
#25843=( BOUNDED_SURFACE ( )  B_SPLINE_SURFACE ( 3, 2, ( 
 ( #22043, #6565, #31680 ),
 ( #18519, #25523, #15644 ),
 ( #3501, #476, #27789 ),
 ( #34570, #5959, #28192 ) ),
 .UNSPECIFIED., .F., .F., .T. ) 
 B_SPLINE_SURFACE_WITH_KNOTS ( ( 4, 4 ),
 ( 3, 3 ),
 ( 0.001168341556843763198, 0.001551611072815416289 ),
 ( 0.000000000000000000, 1.000000000000000000 ),
 .UNSPECIFIED. ) 
 GEOMETRIC_REPRESENTATION_ITEM ( )  RATIONAL_B_SPLINE_SURFACE ( (
 ( 1.000000000000000000, 0.8989970956543276159, 1.000000000000000000),
 ( 1.000000000000000000, 0.8989738193133679500, 1.000000000000000000),
 ( 1.000000000000000000, 0.9033319494950450279, 1.000000000000000000),
 ( 1.000000000000000000, 0.9117915798252654858, 1.000000000000000000) ) ) 
 REPRESENTATION_ITEM ( '' )  SURFACE ( )  );
#25846=AXIS2_PLACEMENT_3D ( 'NONE', #14185, #20368, #1859 ) ;
#25856=ORIENTED_EDGE ( 'NONE', *, *, #40410, .F. ) ;
#25963=CARTESIAN_POINT ( 'NONE',  ( -0.1210148435730033917, -0.5061394519556894345, 0.1438724812234795092 ) ) ;
#25970=CARTESIAN_POINT ( 'NONE',  ( -0.2300000000000000100, 0.5182417262804744906, 0.3749999999999995559 ) ) ;
#25973=CARTESIAN_POINT ( 'NONE',  ( -0.08408070219615658425, -0.09959325338431362917, 0.3599999999999992095 ) ) ;
#26038=CARTESIAN_POINT ( 'NONE',  ( -0.1190701091186160687, -0.4967104654273769571, 0.3286746847624720802 ) ) ;
#26052=CARTESIAN_POINT ( 'NONE',  ( -2.070754768975504589, -0.09959325338431362917, 0.3599999999999976552 ) ) ;
#26078=CARTESIAN_POINT ( 'NONE',  ( -0.2300000000000000100, 0.5182417262804744906, 0.3749999999999995559 ) ) ;
#26118=DIRECTION ( 'NONE',  ( -7.771561172376107616E-16, 7.170354002788761615E-17, -1.000000000000000000 ) ) ;
#26187=CARTESIAN_POINT ( 'NONE',  ( -0.1631212487981059667, 0.5067506594879384041, 0.1120476149576258990 ) ) ;
#26195=( NAMED_UNIT ( * ) PLANE_ANGLE_UNIT ( ) SI_UNIT ( $, .RADIAN. ) );
#26204=ORIENTED_EDGE ( 'NONE', *, *, #2462, .T. ) ;
#26211=VERTEX_POINT ( 'NONE', #22654 ) ;
#26269=CARTESIAN_POINT ( 'NONE',  ( -0.1532354427637373506, 0.4747053032734181999, 0.3600204025348319736 ) ) ;
#26316=VERTEX_POINT ( 'NONE', #11751 ) ;
#26334=CARTESIAN_POINT ( 'NONE',  ( -0.1665334215456128475, 0.5173690063054338095, 0.3289428497172588450 ) ) ;
#26340=AXIS2_PLACEMENT_3D ( 'NONE', #33998, #30907, #30510 ) ;
#26346=AXIS2_PLACEMENT_3D ( 'NONE', #25031, #188, #15769 ) ;
#26347=FACE_OUTER_BOUND ( 'NONE', #31763, .T. ) ;
#26351=CARTESIAN_POINT ( 'NONE',  ( -0.1157108546715127362, -0.4798936717283863174, 0.3382895567580815332 ) ) ;
#26406=DIRECTION ( 'NONE',  ( 0.5794373887239191445, -0.8150167559926640992, 5.613916328591080410E-15 ) ) ;
#26425=CARTESIAN_POINT ( 'NONE',  ( -0.1119307826792291932, -0.5115903042181114690, 0.1085569730127857874 ) ) ;
#26441=DIRECTION ( 'NONE',  ( -7.771561172376107616E-16, 7.170354002788761615E-17, -1.000000000000000000 ) ) ;
#26494=AXIS2_PLACEMENT_3D ( 'NONE', #1276, #23279, #1469 ) ;
#26541=EDGE_CURVE ( 'NONE', #32882, #36405, #40176, .T. ) ;
#26562=AXIS2_PLACEMENT_3D ( 'NONE', #30578, #7986, #21331 ) ;
#26620=AXIS2_PLACEMENT_3D ( 'NONE', #24796, #37316, #31365 ) ;
#26672=AXIS2_PLACEMENT_3D ( 'NONE', #2183, #23596, #11223 ) ;
#26680=DIRECTION ( 'NONE',  ( 1.000000000000000000, 0.000000000000000000, 1.138269997360110167E-15 ) ) ;
#26709=FACE_OUTER_BOUND ( 'NONE', #34968, .T. ) ;
#26781=CARTESIAN_POINT ( 'NONE',  ( -0.1603938765018537715, 0.4636889572247753222, 0.1178658435936994903 ) ) ;
#26828=ORIENTED_EDGE ( 'NONE', *, *, #18200, .F. ) ;
#26857=CARTESIAN_POINT ( 'NONE',  ( -0.1157923916715205420, -0.5295015842444287246, 0.3749999999999992784 ) ) ;
#26872=FACE_OUTER_BOUND ( 'NONE', #30848, .T. ) ;
#26889=VERTEX_POINT ( 'NONE', #12321 ) ;
#26919=CARTESIAN_POINT ( 'NONE',  ( -0.1612862774928046916, 0.5009394326984771828, 0.1071084547150100430 ) ) ;
#26953=ORIENTED_EDGE ( 'NONE', *, *, #11779, .F. ) ;
#26964=ORIENTED_EDGE ( 'NONE', *, *, #20087, .F. ) ;
#26986=DIRECTION ( 'NONE',  ( 0.2828184691484095792, -0.9591734532964046878, 6.102565427610453878E-13 ) ) ;
#27048=CARTESIAN_POINT ( 'NONE',  ( -1.019575837292303166, -0.04310840302197994911, 0.09999999999999879818 ) ) ;
#27049=AXIS2_PLACEMENT_3D ( 'NONE', #15581, #34690, #37369 ) ;
#27061=ORIENTED_EDGE ( 'NONE', *, *, #21244, .F. ) ;
#27091=ADVANCED_FACE ( 'NONE', ( #621 ), #15257, .T. ) ;
#27106=EDGE_CURVE ( 'NONE', #8287, #16786, #183, .T. ) ;
#27111=CYLINDRICAL_SURFACE ( 'NONE', #23247, 2.001674066779348227 ) ;
#27123=CARTESIAN_POINT ( 'NONE',  ( -0.1593650814506384072, 0.4947962564849512357, 0.1029884207726596002 ) ) ;
#27134=CYLINDRICAL_SURFACE ( 'NONE', #24734, 0.03000000000000022787 ) ;
#27142=CIRCLE ( 'NONE', #29092, 0.01499999999999999424 ) ;
#27153=FACE_OUTER_BOUND ( 'NONE', #30420, .T. ) ;
#27245=LINE ( 'NONE', #40581, #38136 ) ;
#27305=AXIS2_PLACEMENT_3D ( 'NONE', #20787, #32892, #14582 ) ;
#27366=DIRECTION ( 'NONE',  ( 7.771561172376107616E-16, -7.170354002788761615E-17, 1.000000000000000000 ) ) ;
#27382=CARTESIAN_POINT ( 'NONE',  ( -0.1178427669581002812, -0.4906303760369221667, 0.1227918960327450820 ) ) ;
#27394=DIRECTION ( 'NONE',  ( -1.000000000000000000, 0.000000000000000000, -1.138269997360103659E-15 ) ) ;
#27439=FACE_OUTER_BOUND ( 'NONE', #8484, .T. ) ;
#27526=DIRECTION ( 'NONE',  ( 1.000000000000000000, 0.000000000000000000, 7.847503847416053677E-16 ) ) ;
#27612=DIRECTION ( 'NONE',  ( 1.000000000000000000, 1.119941574063613413E-31, -7.771561172376107616E-16 ) ) ;
#27630=CIRCLE ( 'NONE', #38124, 0.9087847906030128708 ) ;
#27682=CARTESIAN_POINT ( 'NONE',  ( -0.1167294259372891468, -0.5331983348239500708, 0.1528658435937000626 ) ) ;
#27753=EDGE_CURVE ( 'NONE', #1527, #8287, #11755, .T. ) ;
#27768=CARTESIAN_POINT ( 'NONE',  ( -0.1053653701217057148, -0.4790241930300679352, 0.1089215720160038869 ) ) ;
#27787=EDGE_CURVE ( 'NONE', #12918, #21695, #34988, .T. ) ;
#27789=CARTESIAN_POINT ( 'NONE',  ( -0.1163452666694987092, -0.5320157244525056672, 0.3133290949221909094 ) ) ;
#27819=AXIS2_PLACEMENT_3D ( 'NONE', #8920, #2961, #8315 ) ;
#27828=ORIENTED_EDGE ( 'NONE', *, *, #19314, .F. ) ;
#27854=CARTESIAN_POINT ( 'NONE',  ( -0.1873388932668320073, 0.5325605939836577374, 0.3599999999999993205 ) ) ;
#27897=CARTESIAN_POINT ( 'NONE',  ( -0.1196601186823846308, -0.4996350631411415333, 0.1296977380670712998 ) ) ;
#27939=VERTEX_POINT ( 'NONE', #31695 ) ;
#28028=FACE_OUTER_BOUND ( 'NONE', #17577, .T. ) ;
#28088=DIRECTION ( 'NONE',  ( 7.771561172376107616E-16, -7.170354002788761615E-17, 1.000000000000000000 ) ) ;
#28116=ADVANCED_FACE ( 'NONE', ( #16879 ), #1459, .T. ) ;
#28124=EDGE_CURVE ( 'NONE', #29632, #4981, #6114, .T. ) ;
#28192=CARTESIAN_POINT ( 'NONE',  ( -0.1157923916715135615, -0.5295015842443983045, 0.3181161673586299643 ) ) ;
#28222=ORIENTED_EDGE ( 'NONE', *, *, #30439, .F. ) ;
#28246=( NAMED_UNIT ( * ) SI_UNIT ( $, .STERADIAN. ) SOLID_ANGLE_UNIT ( ) );
#28266=VERTEX_POINT ( 'NONE', #18691 ) ;
#28309=ORIENTED_EDGE ( 'NONE', *, *, #2228, .F. ) ;
#28352=AXIS2_PLACEMENT_3D ( 'NONE', #17617, #30967, #8750 ) ;
#28408=CARTESIAN_POINT ( 'NONE',  ( -0.1210148435730038635, -0.5061394519556884353, 0.1438724812234773442 ) ) ;
#28420=ORIENTED_EDGE ( 'NONE', *, *, #26541, .F. ) ;
#28429=ORIENTED_EDGE ( 'NONE', *, *, #18086, .F. ) ;
#28433=CARTESIAN_POINT ( 'NONE',  ( -0.1707605070207384723, 0.4977265752128581799, 0.1434892898517914628 ) ) ;
#28447=AXIS2_PLACEMENT_3D ( 'NONE', #1040, #26118, #35749 ) ;
#28502=CARTESIAN_POINT ( 'NONE',  ( -0.2300000000000002043, 0.5182417262804744906, 0.08500000000000018652 ) ) ;
#28555=AXIS2_PLACEMENT_3D ( 'NONE', #32378, #36083, #757 ) ;
#28617=CARTESIAN_POINT ( 'NONE',  ( -0.1061036098701634706, -0.4827967145417200179, 0.3599999999999998757 ) ) ;
#28647=ORIENTED_EDGE ( 'NONE', *, *, #33015, .T. ) ;
#28648=CARTESIAN_POINT ( 'NONE',  ( -0.1617315581917542211, 0.4682256792068184570, 0.1178658435936994764 ) ) ;
#28668=CARTESIAN_POINT ( 'NONE',  ( -0.1743922129835733248, -0.5166151207188712791, 0.09999999999999961697 ) ) ;
#28678=ORIENTED_EDGE ( 'NONE', *, *, #25816, .F. ) ;
#28699=TOROIDAL_SURFACE ( 'NONE', #12936, 1.986674066779348768, 0.01499999999999999944 ) ;
#28706=CARTESIAN_POINT ( 'NONE',  ( -0.1133687188271862989, -0.5183431199921479937, 0.3403596628069215368 ) ) ;
#28764=EDGE_CURVE ( 'NONE', #26316, #7093, #2869, .T. ) ;
#28782=FACE_OUTER_BOUND ( 'NONE', #1936, .T. ) ;
#28817=CARTESIAN_POINT ( 'NONE',  ( -1.019575837292303166, -0.04310840302197994911, 0.08499999999999990896 ) ) ;
#28833=B_SPLINE_CURVE_WITH_KNOTS ( 'NONE', 3,
 ( #25561, #28648, #13197, #35006, #3933, #38091, #9910, #28433, #702, #25769 ),
 .UNSPECIFIED., .F., .F.,
 ( 4, 2, 2, 2, 4 ),
 ( 7.269816092101098720E-18, 0.0003553525228749281105, 0.0007107050457498489569, 0.001066057568624769912, 0.001421410091499690758 ),
 .UNSPECIFIED. ) ;
#28853=CARTESIAN_POINT ( 'NONE',  ( -0.1604632851855366527, 0.4983239941852555810, 0.1050370266831589100 ) ) ;
#28861=DIMENSIONAL_EXPONENTS ( 1.000000000000000000, 0.000000000000000000, 0.000000000000000000, 0.000000000000000000, 0.000000000000000000, 0.000000000000000000, 0.000000000000000000 ) ;
#28891=CARTESIAN_POINT ( 'NONE',  ( -0.1154414454259565792, -0.5279056935456777344, 0.3241024189951781653 ) ) ;
#28942=EDGE_LOOP ( 'NONE', ( #857, #33915, #36208, #9713, #10990 ) ) ;
#28948=DIRECTION ( 'NONE',  ( 7.771561172376107616E-16, -7.170354002788761615E-17, 1.000000000000000000 ) ) ;
#28978=EDGE_CURVE ( 'NONE', #31816, #21190, #30368, .T. ) ;
#29005=CARTESIAN_POINT ( 'NONE',  ( -0.1668894944043932960, 0.4852776769345376606, 0.3312153816179764232 ) ) ;
#29050=DIRECTION ( 'NONE',  ( -7.771561172376107616E-16, 7.170354002788761615E-17, -1.000000000000000000 ) ) ;
#29090=AXIS2_PLACEMENT_3D ( 'NONE', #1410, #8162, #17432 ) ;
#29092=AXIS2_PLACEMENT_3D ( 'NONE', #35887, #37772, #6081 ) ;
#29106=CIRCLE ( 'NONE', #29750, 0.9087847906030128708 ) ;
#29137=CARTESIAN_POINT ( 'NONE',  ( -2.070754768975505034, -0.09959325338431362917, 0.1178658435936983939 ) ) ;
#29193=CARTESIAN_POINT ( 'NONE',  ( -0.1073276781670975538, -0.4890918960634569879, 0.09878957693462719902 ) ) ;
#29220=CARTESIAN_POINT ( 'NONE',  ( -0.1688425317846173890, 0.4915896084592923376, 0.3245441658521664996 ) ) ;
#29299=DIRECTION ( 'NONE',  ( -1.000000000000000000, 0.000000000000000000, -7.886895865933756492E-16 ) ) ;
#29355=CYLINDRICAL_SURFACE ( 'NONE', #37540, 0.03000000000000022787 ) ;
#29357=CARTESIAN_POINT ( 'NONE',  ( -0.1522836376793813007, 0.4715211068759145308, 0.3601997132473412355 ) ) ;
#29373=FACE_OUTER_BOUND ( 'NONE', #37230, .T. ) ;
#29401=CARTESIAN_POINT ( 'NONE',  ( -0.1552002433785849012, 0.4812687096812816590, 0.09697487758652631462 ) ) ;
#29421=CARTESIAN_POINT ( 'NONE',  ( -0.1167294259372894244, -0.5331983348239526244, 0.1528658435936947613 ) ) ;
#29434=CARTESIAN_POINT ( 'NONE',  ( -0.1205998369024041117, -0.5041491367644056476, 0.3197686713205454834 ) ) ;
#29458=AXIS2_PLACEMENT_3D ( 'NONE', #570, #31570, #364 ) ;
#29464=DIRECTION ( 'NONE',  ( 1.000000000000000000, 0.000000000000000000, 7.588466649067360358E-16 ) ) ;
#29487=ORIENTED_EDGE ( 'NONE', *, *, #33818, .F. ) ;
#29505=CARTESIAN_POINT ( 'NONE',  ( -0.1137534828624003069, -0.5201328034396339728, 0.1183403147931640503 ) ) ;
#29566=CIRCLE ( 'NONE', #6641, 0.9087847906030128708 ) ;
#29582=VERTEX_POINT ( 'NONE', #23841 ) ;
#29591=CARTESIAN_POINT ( 'NONE',  ( -0.1508021419688959364, 0.4665171419162750799, 0.1089215716837025061 ) ) ;
#29632=VERTEX_POINT ( 'NONE', #33472 ) ;
#29637=EDGE_CURVE ( 'NONE', #21878, #38042, #21290, .T. ) ;
#29662=CARTESIAN_POINT ( 'NONE',  ( -0.1684323895664684156, 0.5231977504175356897, 0.1528658435937000626 ) ) ;
#29680=AXIS2_PLACEMENT_3D ( 'NONE', #19402, #31937, #3755 ) ;
#29705=CARTESIAN_POINT ( 'NONE',  ( -0.1104192559602709262, -0.5043764815743676522, 0.1033498972402041999 ) ) ;
#29745=ORIENTED_EDGE ( 'NONE', *, *, #39296, .F. ) ;
#29750=AXIS2_PLACEMENT_3D ( 'NONE', #38211, #28948, #35520 ) ;
#29770=CIRCLE ( 'NONE', #12036, 0.04500000000000022038 ) ;
#29772=CARTESIAN_POINT ( 'NONE',  ( -0.1710642718812830643, 0.4986889572247755198, 0.3032895567580806695 ) ) ;
#29785=CARTESIAN_POINT ( 'NONE',  ( -1.019575837292303166, -0.04310840302197994911, 0.3749999999999990008 ) ) ;
#29816=AXIS2_PLACEMENT_3D ( 'NONE', #4866, #1036, #39433 ) ;
#29818=CARTESIAN_POINT ( 'NONE',  ( -0.1167294259372883281, -0.5331983348239501819, 0.3032895567580801144 ) ) ;
#29823=CARTESIAN_POINT ( 'NONE',  ( -0.1684323895665172655, 0.5231977504176978933, 0.3102582297535276257 ) ) ;
#29830=AXIS2_PLACEMENT_3D ( 'NONE', #2232, #1837, #27526 ) ;
#29835=DIRECTION ( 'NONE',  ( -7.771561172376107616E-16, 7.170354002788761615E-17, -1.000000000000000000 ) ) ;
#29839=CARTESIAN_POINT ( 'NONE',  ( -0.1210148435730253880, -0.5061394519557965710, 0.3122829191278980177 ) ) ;
#29842=EDGE_LOOP ( 'NONE', ( #22297, #38341, #39252, #20165 ) ) ;
#29851=ORIENTED_EDGE ( 'NONE', *, *, #30439, .T. ) ;
#29861=AXIS2_PLACEMENT_3D ( 'NONE', #36683, #8489, #21050 ) ;
#29896=EDGE_LOOP ( 'NONE', ( #2326, #22521, #21537, #26828 ) ) ;
#29923=VERTEX_POINT ( 'NONE', #4617 ) ;
#29933=EDGE_CURVE ( 'NONE', #39260, #29582, #19963, .T. ) ;
#30006=CARTESIAN_POINT ( 'NONE',  ( -0.1623906354757041204, 0.5045448597005471880, 0.1308137833173686204 ) ) ;
#30066=VERTEX_POINT ( 'NONE', #25196 ) ;
#30076=DIRECTION ( 'NONE',  ( 1.000000000000000000, 0.000000000000000000, 7.762739824594491602E-16 ) ) ;
#30080=CARTESIAN_POINT ( 'NONE',  ( -0.1157923916715205420, -0.5295015842444287246, 0.3749999999999992784 ) ) ;
#30096=DIRECTION ( 'NONE',  ( -3.406373435249024214E-19, -1.000000000000000000, -7.170354002788761615E-17 ) ) ;
#30155=CARTESIAN_POINT ( 'NONE',  ( -0.1142670043590668094, -0.4723146173917492918, 0.3382895567580812557 ) ) ;
#30156=EDGE_LOOP ( 'NONE', ( #14820, #32480, #5601, #30514, #39542, #32007 ) ) ;
#30195=CARTESIAN_POINT ( 'NONE',  ( -0.1529829672178498190, 0.4739133692255307895, 0.09550516375514117584 ) ) ;
#30212=CARTESIAN_POINT ( 'NONE',  ( -0.1684323895664520399, 0.5231977504174887272, 0.3032895567580809471 ) ) ;
#30213=CARTESIAN_POINT ( 'NONE',  ( -0.1679391139942039701, 0.5216964164669857240, 0.3184569295944739142 ) ) ;
#30279=DIRECTION ( 'NONE',  ( -7.771561172376107616E-16, 7.170354002788761615E-17, -1.000000000000000000 ) ) ;
#30297=EDGE_CURVE ( 'NONE', #26211, #38543, #10782, .T. ) ;
#30368=B_SPLINE_CURVE_WITH_KNOTS ( 'NONE', 3,
 ( #29662, #13023, #38101, #31944, #35015, #3764, #26187, #28853, #25781, #10349 ),
 .UNSPECIFIED., .F., .F.,
 ( 4, 2, 2, 2, 4 ),
 ( 6.071532165919065186E-18, 0.0004362256165457094434, 0.0008724512330914128153, 0.001308676849637116241, 0.001744902466182819559 ),
 .UNSPECIFIED. ) ;
#30399=AXIS2_PLACEMENT_3D ( 'NONE', #28502, #12879, #19652 ) ;
#30420=EDGE_LOOP ( 'NONE', ( #11831, #18, #35449, #33374, #3690 ) ) ;
#30439=EDGE_CURVE ( 'NONE', #21190, #7716, #21497, .T. ) ;
#30481=DIRECTION ( 'NONE',  ( 0.9591734532964046878, 0.2828184691484092461, 0.000000000000000000 ) ) ;
#30492=AXIS2_PLACEMENT_3D ( 'NONE', #14800, #27366, #39891 ) ;
#30510=DIRECTION ( 'NONE',  ( 1.000000000000000000, 1.119941574063613413E-31, -7.771561172376107616E-16 ) ) ;
#30514=ORIENTED_EDGE ( 'NONE', *, *, #20539, .T. ) ;
#30543=EDGE_CURVE ( 'NONE', #12799, #4767, #4237, .T. ) ;
#30578=CARTESIAN_POINT ( 'NONE',  ( -0.2300000000000002043, 0.5182417262804744906, 0.08500000000000018652 ) ) ;
#30586=FACE_OUTER_BOUND ( 'NONE', #16100, .T. ) ;
#30639=CARTESIAN_POINT ( 'NONE',  ( -0.1638630105339158594, 0.5092090815894317890, 0.3148090297061104104 ) ) ;
#30646=EDGE_CURVE ( 'NONE', #16211, #26211, #28833, .T. ) ;
#30653=CARTESIAN_POINT ( 'NONE',  ( -0.2043922129835732682, -0.5166151207188712791, 0.08499999999999961753 ) ) ;
#30687=DIRECTION ( 'NONE',  ( 7.771561172376107616E-16, -7.170354002788761615E-17, 1.000000000000000000 ) ) ;
#30752=ORIENTED_EDGE ( 'NONE', *, *, #40586, .T. ) ;
#30779=EDGE_LOOP ( 'NONE', ( #26964, #28309, #28420, #12146, #2980 ) ) ;
#30813=FACE_OUTER_BOUND ( 'NONE', #30156, .T. ) ;
#30828=CARTESIAN_POINT ( 'NONE',  ( -0.1795773455677812658, 0.4580325878418074481, 0.09550516381870167992 ) ) ;
#30830=CARTESIAN_POINT ( 'NONE',  ( -0.1212602504878774051, -0.5073146173917495450, 0.3032895567580812246 ) ) ;
#30848=EDGE_LOOP ( 'NONE', ( #3921, #34132, #8036 ) ) ;
#30849=CARTESIAN_POINT ( 'NONE',  ( -0.2343922129835731283, -0.5166151207188712791, 0.3750000000000000555 ) ) ;
#30850=ORIENTED_EDGE ( 'NONE', *, *, #17808, .T. ) ;
#30907=DIRECTION ( 'NONE',  ( 7.771561172376107616E-16, -7.170354002788761615E-17, 1.000000000000000000 ) ) ;
#30967=DIRECTION ( 'NONE',  ( -7.771561172376107616E-16, 7.170354002788761615E-17, -1.000000000000000000 ) ) ;
#30968=LINE ( 'NONE', #40631, #16559 ) ;
#31001=CIRCLE ( 'NONE', #13932, 2.001558204291726373 ) ;
#31002=ORIENTED_EDGE ( 'NONE', *, *, #14497, .F. ) ;
#31120=ORIENTED_EDGE ( 'NONE', *, *, #36897, .F. ) ;
#31130=CIRCLE ( 'NONE', #24558, 0.04500000000000030365 ) ;
#31191=VECTOR ( 'NONE', #11455, 39.37007874015748143 ) ;
#31235=CARTESIAN_POINT ( 'NONE',  ( -0.6247879186461519074, 0.2375666616292472499, 0.3749999999999995559 ) ) ;
#31337=CARTESIAN_POINT ( 'NONE',  ( -0.1574377185082707353, 0.4885537809602777948, 0.09999999999999989453 ) ) ;
#31341=TOROIDAL_SURFACE ( 'NONE', #13593, 1.986674066779348768, 0.01499999999999999944 ) ;
#31365=DIRECTION ( 'NONE',  ( 1.000000000000000000, 2.042862361497887782E-14, 7.734859593387037307E-16 ) ) ;
#31376=DIRECTION ( 'NONE',  ( 1.000000000000000000, 1.113825344428167933E-31, -7.771561172376107616E-16 ) ) ;
#31387=EDGE_CURVE ( 'NONE', #15152, #17948, #12828, .T. ) ;
#31539=DIRECTION ( 'NONE',  ( -1.000000000000000000, 0.000000000000000000, -7.762644838731319154E-16 ) ) ;
#31570=DIRECTION ( 'NONE',  ( 0.5794373887239150367, -0.8150167559926670968, 2.848458103903287201E-16 ) ) ;
#31573=ORIENTED_EDGE ( 'NONE', *, *, #25336, .F. ) ;
#31680=CARTESIAN_POINT ( 'NONE',  ( -0.1167294259372889248, -0.5331983348239512921, 0.3032895567580763396 ) ) ;
#31688=CIRCLE ( 'NONE', #23800, 0.9237847906030128842 ) ;
#31691=CIRCLE ( 'NONE', #8004, 0.03000000000000002318 ) ;
#31695=CARTESIAN_POINT ( 'NONE',  ( -0.1107910466892899765, -0.04310840302197994911, 0.3599999999999985989 ) ) ;
#31723=CIRCLE ( 'NONE', #24512, 0.02999999999999999195 ) ;
#31763=EDGE_LOOP ( 'NONE', ( #2984, #8942, #729, #8638, #23995, #32616, #26204, #11778 ) ) ;
#31787=CARTESIAN_POINT ( 'NONE',  ( -0.1093417548587973798, -0.4991680509864717674, 0.3564048400776359538 ) ) ;
#31805=DIRECTION ( 'NONE',  ( 3.414809992080326361E-15, 1.000000000000000000, -2.845674993400271967E-15 ) ) ;
#31816=VERTEX_POINT ( 'NONE', #7175 ) ;
#31875=CARTESIAN_POINT ( 'NONE',  ( -0.1304423469995338869, -0.5262799683630393632, 0.09999999999999933942 ) ) ;
#31916=CIRCLE ( 'NONE', #34556, 0.06000000000000021289 ) ;
#31937=DIRECTION ( 'NONE',  ( 7.771561172376107616E-16, -7.170354002788761615E-17, 1.000000000000000000 ) ) ;
#31944=CARTESIAN_POINT ( 'NONE',  ( -0.1670982076487625978, 0.5191099701766067609, 0.1307156235296936808 ) ) ;
#31948=CARTESIAN_POINT ( 'NONE',  ( -0.1107910466892899765, -0.04310840302197994911, 0.09999999999999809042 ) ) ;
#31976=B_SPLINE_CURVE_WITH_KNOTS ( 'NONE', 3,
 ( #20105, #16813, #29357, #13702, #1198, #26269, #10420 ),
 .UNSPECIFIED., .F., .F.,
 ( 4, 3, 4 ),
 ( 0.000000000000000000, 0.0001987961317490854899, 0.0002262042107145686282 ),
 .UNSPECIFIED. ) ;
#31988=CARTESIAN_POINT ( 'NONE',  ( -0.1148620258665340038, -0.5252635219643339015, 0.3299751171063038946 ) ) ;
#32007=ORIENTED_EDGE ( 'NONE', *, *, #12448, .T. ) ;
#32046=MANIFOLD_SOLID_BREP ( 'Fillet2', #32579 ) ;
#32068=ORIENTED_EDGE ( 'NONE', *, *, #36088, .F. ) ;
#32105=EDGE_CURVE ( 'NONE', #7716, #16211, #20380, .T. ) ;
#32118=DIRECTION ( 'NONE',  ( -1.000000000000000000, 0.000000000000000000, 0.000000000000000000 ) ) ;
#32138=ORIENTED_EDGE ( 'NONE', *, *, #30646, .T. ) ;
#32143=CARTESIAN_POINT ( 'NONE',  ( -0.1339136704200473982, -0.4685718226220191851, 0.3606502365330779836 ) ) ;
#32156=CARTESIAN_POINT ( 'NONE',  ( -0.2300000000000000100, 0.5182417262804744906, 0.3749999999999995559 ) ) ;
#32229=AXIS2_PLACEMENT_3D ( 'NONE', #13418, #15689, #12819 ) ;
#32249=TOROIDAL_SURFACE ( 'NONE', #10561, 1.986674066779348768, 0.01499999999999999944 ) ;
#32284=CARTESIAN_POINT ( 'NONE',  ( -0.1631341089705869718, 0.4729174206798188451, 0.3373594846482096399 ) ) ;
#32318=AXIS2_PLACEMENT_3D ( 'NONE', #35609, #3748, #12803 ) ;
#32359=CARTESIAN_POINT ( 'NONE',  ( -2.070754768975505034, -0.09959325338431362917, 0.3749999999999976130 ) ) ;
#32378=CARTESIAN_POINT ( 'NONE',  ( -2.070754768975505034, -0.09959325338431362917, 0.1178658435936983939 ) ) ;
#32480=ORIENTED_EDGE ( 'NONE', *, *, #23552, .T. ) ;
#32493=AXIS2_PLACEMENT_3D ( 'NONE', #36214, #8029, #33137 ) ;
#32513=FACE_OUTER_BOUND ( 'NONE', #2297, .T. ) ;
#32564=DIRECTION ( 'NONE',  ( 1.000000000000000000, 0.000000000000000000, 1.517693329813469311E-15 ) ) ;
#32579=CLOSED_SHELL ( 'NONE', ( #17521, #22345, #39848, #33466, #6475, #40084, #5414, #8973, #17102, #16248, #21105, #9259, #7201, #10766, #8994, #19982, #25526, #40385, #7619, #39188, #37961, #1732, #25030, #2753, #13701, #27091, #8694, #22136, #15925, #20727, #24781, #13188, #24039, #28116, #33270, #23366, #4179, #1360, #9937 ) ) ;
#32596=CIRCLE ( 'NONE', #1772, 0.03000000000000000583 ) ;
#32616=ORIENTED_EDGE ( 'NONE', *, *, #22000, .T. ) ;
#32641=DIRECTION ( 'NONE',  ( 1.000000000000000000, 1.131052719138050089E-31, -7.771561172376107616E-16 ) ) ;
#32819=ORIENTED_EDGE ( 'NONE', *, *, #20999, .F. ) ;
#32868=CARTESIAN_POINT ( 'NONE',  ( -0.1524980003306027898, 0.4722686132664294933, 0.1089215716291629665 ) ) ;
#32871=DIRECTION ( 'NONE',  ( 1.000000000000000000, 0.000000000000000000, 7.906745362128971688E-16 ) ) ;
#32882=VERTEX_POINT ( 'NONE', #8261 ) ;
#32892=DIRECTION ( 'NONE',  ( 7.771561172376107616E-16, -7.170354002788761615E-17, 1.000000000000000000 ) ) ;
#32904=CIRCLE ( 'NONE', #26346, 0.02999999999999996073 ) ;
#33014=FACE_OUTER_BOUND ( 'NONE', #37014, .T. ) ;
#33015=EDGE_CURVE ( 'NONE', #15711, #39260, #38064, .T. ) ;
#33029=DIRECTION ( 'NONE',  ( -1.000000000000000000, 0.000000000000000000, 0.000000000000000000 ) ) ;
#33063=( GEOMETRIC_REPRESENTATION_CONTEXT ( 3 ) GLOBAL_UNCERTAINTY_ASSIGNED_CONTEXT ( ( #13265 ) ) GLOBAL_UNIT_ASSIGNED_CONTEXT ( ( #925, #9530, #28246 ) ) REPRESENTATION_CONTEXT ( 'NONE', 'WORKASPACE' ) );
#33080=CARTESIAN_POINT ( 'NONE',  ( -0.1646294012188420086, 0.5114631038222653414, 0.1176773486970827121 ) ) ;
#33114=CIRCLE ( 'NONE', #37723, 0.06000000000000021289 ) ;
#33120=CARTESIAN_POINT ( 'NONE',  ( -0.1142670043590668094, -0.4723146173917492918, 0.3382895567580812557 ) ) ;
#33124=ORIENTED_EDGE ( 'NONE', *, *, #21002, .F. ) ;
#33137=DIRECTION ( 'NONE',  ( 1.000000000000000000, 7.194105162071894010E-14, 7.847494366974321282E-16 ) ) ;
#33270=ADVANCED_FACE ( 'NONE', ( #69 ), #24050, .T. ) ;
#33287=ORIENTED_EDGE ( 'NONE', *, *, #11779, .T. ) ;
#33311=CARTESIAN_POINT ( 'NONE',  ( -0.2299999999999999267, 0.5182417262804744906, 0.09999999999999989453 ) ) ;
#33338=CARTESIAN_POINT ( 'NONE',  ( -0.1617138679863628359, 0.4681656832120535405, 0.3382895567580768703 ) ) ;
#33374=ORIENTED_EDGE ( 'NONE', *, *, #4170, .F. ) ;
#33446=DIRECTION ( 'NONE',  ( 1.000000000000000000, 1.113825344428167933E-31, -7.771561172376107616E-16 ) ) ;
#33466=ADVANCED_FACE ( 'NONE', ( #20976 ), #36415, .T. ) ;
#33472=CARTESIAN_POINT ( 'NONE',  ( -0.2043922129835731294, -0.5166151207188712791, 0.3750000000000001110 ) ) ;
#33489=DIRECTION ( 'NONE',  ( 0.9591734532964094617, 0.2828184691483933699, 5.691349986800551823E-16 ) ) ;
#33512=AXIS2_PLACEMENT_3D ( 'NONE', #5753, #33732, #11924 ) ;
#33634=AXIS2_PLACEMENT_3D ( 'NONE', #2502, #40119, #8865 ) ;
#33675=ORIENTED_EDGE ( 'NONE', *, *, #2228, .T. ) ;
#33688=CARTESIAN_POINT ( 'NONE',  ( -0.1088121136105147380, -0.4964308608213456875, 0.09999999999999989453 ) ) ;
#33710=CARTESIAN_POINT ( 'NONE',  ( -0.1707812261971881906, 0.4977922652119479152, 0.3123933982393728437 ) ) ;
#33730=CARTESIAN_POINT ( 'NONE',  ( -0.1133606652272154125, -0.5183057948313382068, 0.1157398326556813989 ) ) ;
#33732=DIRECTION ( 'NONE',  ( 0.3181970600707382246, -0.9480245940703960761, 3.970578237956065974E-16 ) ) ;
#33746=CARTESIAN_POINT ( 'NONE',  ( -0.1696273608102555064, 0.4941101834779049740, 0.3212105875170800373 ) ) ;
#33818=EDGE_CURVE ( 'NONE', #29632, #35323, #10542, .T. ) ;
#33852=AXIS2_PLACEMENT_3D ( 'NONE', #15337, #18219, #40626 ) ;
#33880=DIRECTION ( 'NONE',  ( 1.000000000000000000, 0.000000000000000000, 8.537024980200777445E-16 ) ) ;
#33915=ORIENTED_EDGE ( 'NONE', *, *, #9532, .F. ) ;
#33927=EDGE_LOOP ( 'NONE', ( #28429, #9230 ) ) ;
#33933=CARTESIAN_POINT ( 'NONE',  ( -0.1210963378865855811, -0.5065302875297102991, 0.3108129518247090828 ) ) ;
#33950=CARTESIAN_POINT ( 'NONE',  ( -0.1044436713285742391, -0.4741860147765890043, 0.1089215716837025894 ) ) ;
#33964=DIRECTION ( 'NONE',  ( 0.9823333030490228879, -0.1871397384865027547, 5.691349986800549851E-16 ) ) ;
#33988=DIRECTION ( 'NONE',  ( -7.771561172376107616E-16, 7.170354002788761615E-17, -1.000000000000000000 ) ) ;
#33998=CARTESIAN_POINT ( 'NONE',  ( -2.070754768975504589, -0.09959325338431362917, 0.3599999999999976552 ) ) ;
#34091=CARTESIAN_POINT ( 'NONE',  ( -0.1684323895664702475, 0.5231977504175419069, 0.1528658435937316484 ) ) ;
#34115=EDGE_CURVE ( 'NONE', #12918, #9065, #18034, .T. ) ;
#34132=ORIENTED_EDGE ( 'NONE', *, *, #36612, .T. ) ;
#34195=VERTEX_POINT ( 'NONE', #4108 ) ;
#34227=CIRCLE ( 'NONE', #13867, 0.01499999999999997689 ) ;
#34242=DIRECTION ( 'NONE',  ( -7.771561172376107616E-16, 7.170354002788761615E-17, -1.000000000000000000 ) ) ;
#34322=DIRECTION ( 'NONE',  ( -7.771561172376107616E-16, 7.170354002788761615E-17, -1.000000000000000000 ) ) ;
#34338=CARTESIAN_POINT ( 'NONE',  ( -0.1056392956507359038, -0.4804620820570907891, 0.09550516425342367444 ) ) ;
#34410=AXIS2_PLACEMENT_3D ( 'NONE', #38236, #22639, #22427 ) ;
#34424=EDGE_CURVE ( 'NONE', #15629, #22311, #21278, .T. ) ;
#34519=ORIENTED_EDGE ( 'NONE', *, *, #16014, .F. ) ;
#34556=AXIS2_PLACEMENT_3D ( 'NONE', #28668, #6836, #19001 ) ;
#34570=CARTESIAN_POINT ( 'NONE',  ( -0.1210148435730243194, -0.5061394519557864680, 0.3122829191279359318 ) ) ;
#34573=VERTEX_POINT ( 'NONE', #18436 ) ;
#34638=CARTESIAN_POINT ( 'NONE',  ( -2.070754768975505034, -0.09959325338431362917, 0.09813923389047245205 ) ) ;
#34655=DIRECTION ( 'NONE',  ( -7.771561172376107616E-16, 7.170354002788761615E-17, -1.000000000000000000 ) ) ;
#34690=DIRECTION ( 'NONE',  ( -7.771561172376107616E-16, 7.170354002788761615E-17, -1.000000000000000000 ) ) ;
#34705=CIRCLE ( 'NONE', #29458, 0.01500000000000001679 ) ;
#34709=DIRECTION ( 'NONE',  ( 7.771561172376107616E-16, -7.170354002788761615E-17, 1.000000000000000000 ) ) ;
#34721=DIRECTION ( 'NONE',  ( 1.000000000000000000, 1.131052719138050089E-31, -7.771561172376107616E-16 ) ) ;
#34823=( BOUNDED_SURFACE ( )  B_SPLINE_SURFACE ( 3, 2, ( 
 ( #40518, #33950, #5751 ),
 ( #40307, #27768, #34338 ),
 ( #12137, #5543, #2280 ),
 ( #11728, #14819, #5322 ),
 ( #27382, #15213, #39908 ),
 ( #2672, #42, #36807 ),
 ( #8841, #24699, #33730 ),
 ( #12340, #37231, #9049 ),
 ( #6153, #21191, #21611 ),
 ( #15630, #24898, #2479 ) ),
 .UNSPECIFIED., .F., .F., .F. ) 
 B_SPLINE_SURFACE_WITH_KNOTS ( ( 4, 2, 2, 2, 4 ),
 ( 3, 3 ),
 ( 0.001500576079630530895, 0.001976458225352494859, 0.002452340371074459256, 0.002928222516796423220, 0.003404104662518387184 ),
 ( 0.000000000000000000, 1.000000000000000000 ),
 .UNSPECIFIED. ) 
 GEOMETRIC_REPRESENTATION_ITEM ( )  RATIONAL_B_SPLINE_SURFACE ( (
 ( 1.000000000000000000, 0.9128709291752995503, 1.000000000000000000),
 ( 1.000000000000000000, 0.9128711300566455522, 1.000000000000000000),
 ( 1.000000000000000000, 0.9128295461284150480, 1.000000000000000000),
 ( 1.000000000000000000, 0.9126769222980595231, 1.000000000000000000),
 ( 1.000000000000000000, 0.9125696619638158369, 1.000000000000000000),
 ( 1.000000000000000000, 0.9123247991092858777, 1.000000000000000000),
 ( 1.000000000000000000, 0.9121939566647505604, 1.000000000000000000),
 ( 1.000000000000000000, 0.9119567588128756341, 1.000000000000000000),
 ( 1.000000000000000000, 0.9118559517120560232, 1.000000000000000000),
 ( 1.000000000000000000, 0.9117915798251829962, 1.000000000000000000) ) ) 
 REPRESENTATION_ITEM ( '' )  SURFACE ( )  );
#34859=CARTESIAN_POINT ( 'NONE',  ( -0.1142670043590661988, -0.4723146173917421309, 0.3382895567580809226 ) ) ;
#34888=FACE_OUTER_BOUND ( 'NONE', #28942, .T. ) ;
#34968=EDGE_LOOP ( 'NONE', ( #7922, #19646, #13111, #2872, #5292, #40038 ) ) ;
#34973=CIRCLE ( 'NONE', #33634, 0.03000000000000022787 ) ;
#34974=CIRCLE ( 'NONE', #864, 0.03000000000000022787 ) ;
#34981=CARTESIAN_POINT ( 'NONE',  ( -0.1873388932668322848, 0.5325605939836577374, 0.08500000000000018652 ) ) ;
#34988=CIRCLE ( 'NONE', #40237, 0.02999999999999998848 ) ;
#35006=CARTESIAN_POINT ( 'NONE',  ( -0.1655961216393919966, 0.4810575411953317282, 0.1221435944151032377 ) ) ;
#35015=CARTESIAN_POINT ( 'NONE',  ( -0.1663058949915988405, 0.5166728756553480295, 0.1255325300626448648 ) ) ;
#35023=CIRCLE ( 'NONE', #6796, 0.01499999999999997863 ) ;
#35041=AXIS2_PLACEMENT_3D ( 'NONE', #3812, #23165, #31805 ) ;
#35063=B_SPLINE_CURVE_WITH_KNOTS ( 'NONE', 3,
 ( #33120, #26351, #4517, #17495, #29434, #29839 ),
 .UNSPECIFIED., .F., .F.,
 ( 4, 2, 4 ),
 ( 0.002802047142276813813, 0.003388785079928784139, 0.003975523017580754465 ),
 .UNSPECIFIED. ) ;
#35081=CARTESIAN_POINT ( 'NONE',  ( -0.1061036098701634706, -0.4827967145417200179, 0.3599999999999998757 ) ) ;
#35117=ORIENTED_EDGE ( 'NONE', *, *, #9756, .T. ) ;
#35175=ORIENTED_EDGE ( 'NONE', *, *, #1321, .T. ) ;
#35198=CARTESIAN_POINT ( 'NONE',  ( -0.1508021419688934661, 0.4665171419162789102, 0.3472338286680812791 ) ) ;
#35221=AXIS2_PLACEMENT_3D ( 'NONE', #23216, #14137, #36344 ) ;
#35278=CARTESIAN_POINT ( 'NONE',  ( -0.1208133668958378537, -0.5051731972035429230, 0.3159170889047719366 ) ) ;
#35323=VERTEX_POINT ( 'NONE', #30653 ) ;
#35381=EDGE_LOOP ( 'NONE', ( #8144, #9750, #10576, #12848, #32138, #36929, #14493, #264, #2478, #24302, #17550 ) ) ;
#35389=CARTESIAN_POINT ( 'NONE',  ( -0.1696286242763865582, 0.4941126639394797793, 0.3207424310465874506 ) ) ;
#35449=ORIENTED_EDGE ( 'NONE', *, *, #14752, .F. ) ;
#35451=ORIENTED_EDGE ( 'NONE', *, *, #25654, .T. ) ;
#35502=VERTEX_POINT ( 'NONE', #9384 ) ;
#35504=LINE ( 'NONE', #1011, #11213 ) ;
#35508=TOROIDAL_SURFACE ( 'NONE', #26340, 1.986674066779348768, 0.01499999999999999944 ) ;
#35520=DIRECTION ( 'NONE',  ( 1.000000000000000000, 0.000000000000000000, 7.515112548955565209E-16 ) ) ;
#35544=APPLICATION_CONTEXT ( 'configuration controlled 3d designs of mechanical parts and assemblies' ) ;
#35547=VECTOR ( 'NONE', #20702, 39.37007874015748143 ) ;
#35570=TOROIDAL_SURFACE ( 'NONE', #25718, 0.9237847906030132172, 0.01499999999999999944 ) ;
#35581=CARTESIAN_POINT ( 'NONE',  ( -0.1589247078932900514, 0.4934387919092068087, 0.3384493358270272978 ) ) ;
#35582=AXIS2_PLACEMENT_3D ( 'NONE', #21436, #39717, #33964 ) ;
#35609=CARTESIAN_POINT ( 'NONE',  ( -0.2300000000000000100, 0.5182417262804744906, 0.3749999999999995559 ) ) ;
#35630=DIRECTION ( 'NONE',  ( 0.9823333030490228879, -0.1871397384865027547, 0.000000000000000000 ) ) ;
#35646=EDGE_CURVE ( 'NONE', #19133, #37952, #36381, .T. ) ;
#35651=DIRECTION ( 'NONE',  ( 7.771561172376107616E-16, -7.170354002788761615E-17, 1.000000000000000000 ) ) ;
#35661=ORIENTED_EDGE ( 'NONE', *, *, #11197, .T. ) ;
#35749=DIRECTION ( 'NONE',  ( 1.000000000000000000, 0.000000000000000000, 1.138269997360105631E-15 ) ) ;
#35807=VERTEX_POINT ( 'NONE', #4691 ) ;
#35887=CARTESIAN_POINT ( 'NONE',  ( -0.09579104668929040722, -0.04310840302197994911, 0.09999999999999951983 ) ) ;
#35897=DIRECTION ( 'NONE',  ( -7.771561172376107616E-16, 7.170354002788761615E-17, -1.000000000000000000 ) ) ;
#35929=ORIENTED_EDGE ( 'NONE', *, *, #1902, .T. ) ;
#35941=VERTEX_POINT ( 'NONE', #25210 ) ;
#35973=CARTESIAN_POINT ( 'NONE',  ( -0.1656815030311133141, 0.4813244629265694408, 0.1225468705240552458 ) ) ;
#36007=ORIENTED_EDGE ( 'NONE', *, *, #20230, .T. ) ;
#36065=ORIENTED_EDGE ( 'NONE', *, *, #22000, .F. ) ;
#36083=DIRECTION ( 'NONE',  ( 7.771561172376107616E-16, -7.170354002788761615E-17, 1.000000000000000000 ) ) ;
#36088=EDGE_CURVE ( 'NONE', #35941, #12958, #10163, .T. ) ;
#36100=ORIENTED_EDGE ( 'NONE', *, *, #628, .T. ) ;
#36106=DIRECTION ( 'NONE',  ( -1.252096997096119587E-14, 1.000000000000000000, -2.162712994984206616E-14 ) ) ;
#36163=CARTESIAN_POINT ( 'NONE',  ( -0.1638606670177130409, 0.5090623078239890908, 0.1147396705136482370 ) ) ;
#36186=CARTESIAN_POINT ( 'NONE',  ( -0.1212602505242198897, -0.5073146173415499227, 0.1498414178977029720 ) ) ;
#36208=ORIENTED_EDGE ( 'NONE', *, *, #29637, .F. ) ;
#36214=CARTESIAN_POINT ( 'NONE',  ( -2.070754768975504589, -0.09959325338431362917, 0.3599999999999976552 ) ) ;
#36219=CARTESIAN_POINT ( 'NONE',  ( -0.1688017273025779752, 0.4914669153062978801, 0.3250764289764314086 ) ) ;
#36273=ORIENTED_EDGE ( 'NONE', *, *, #5929, .F. ) ;
#36342=CIRCLE ( 'NONE', #28447, 0.06000000000000021289 ) ;
#36344=DIRECTION ( 'NONE',  ( 0.000000000000000000, 0.000000000000000000, -1.000000000000000000 ) ) ;
#36351=CARTESIAN_POINT ( 'NONE',  ( -0.1055448275397413149, -0.4799318856336941552, 0.3601683063145866837 ) ) ;
#36381=CIRCLE ( 'NONE', #26562, 0.04500000000000030365 ) ;
#36405=VERTEX_POINT ( 'NONE', #6829 ) ;
#36415=TOROIDAL_SURFACE ( 'NONE', #30492, 0.9237847906030132172, 0.01499999999999999944 ) ;
#36423=EDGE_CURVE ( 'NONE', #22311, #35502, #1644, .T. ) ;
#36480=ORIENTED_EDGE ( 'NONE', *, *, #31387, .F. ) ;
#36514=DIRECTION ( 'NONE',  ( 1.000000000000000000, 0.000000000000000000, 1.138269997360110167E-15 ) ) ;
#36565=EDGE_CURVE ( 'NONE', #29923, #19133, #17387, .T. ) ;
#36567=AXIS2_PLACEMENT_3D ( 'NONE', #27048, #11410, #1779 ) ;
#36581=CARTESIAN_POINT ( 'NONE',  ( -0.1628171590788805023, 0.5058980335669727157, 0.1333422639292590750 ) ) ;
#36612=EDGE_CURVE ( 'NONE', #51, #40488, #18878, .T. ) ;
#36678=ORIENTED_EDGE ( 'NONE', *, *, #13909, .F. ) ;
#36683=CARTESIAN_POINT ( 'NONE',  ( -0.1304423469995333318, -0.5262799683630392522, 0.3599999999999987654 ) ) ;
#36807=CARTESIAN_POINT ( 'NONE',  ( -0.1124521194441415461, -0.5140518175048249816, 0.1111873348898669150 ) ) ;
#36823=EDGE_CURVE ( 'NONE', #30066, #29582, #7048, .T. ) ;
#36874=CARTESIAN_POINT ( 'NONE',  ( -0.1530923209794372852, 0.4738745695581291772, 0.09813923389054934887 ) ) ;
#36897=EDGE_CURVE ( 'NONE', #9709, #17150, #23758, .T. ) ;
#36907=DIRECTION ( 'NONE',  ( -7.771561172376107616E-16, 7.170354002788761615E-17, -1.000000000000000000 ) ) ;
#36929=ORIENTED_EDGE ( 'NONE', *, *, #30297, .T. ) ;
#36947=CARTESIAN_POINT ( 'NONE',  ( -0.6247879186461520185, 0.2375666616292472499, 0.08499999999999936773 ) ) ;
#36953=VECTOR ( 'NONE', #14850, 39.37007874015748143 ) ;
#36979=DIRECTION ( 'NONE',  ( -7.771561172376097755E-16, -7.170354002788760383E-17, 1.000000000000000000 ) ) ;
#36986=DIRECTION ( 'NONE',  ( -1.000000000000000000, 0.000000000000000000, 0.000000000000000000 ) ) ;
#37014=EDGE_LOOP ( 'NONE', ( #11206, #30752, #2830, #22479 ) ) ;
#37036=CARTESIAN_POINT ( 'NONE',  ( -0.1707627412572580439, 0.4977336986496906923, 0.3126474374754089625 ) ) ;
#37055=CARTESIAN_POINT ( 'NONE',  ( -2.070754768975505034, -0.09959325338431362917, 0.3382895567580804230 ) ) ;
#37159=CARTESIAN_POINT ( 'NONE',  ( -0.1743922129835729085, -0.5166151207188712791, 0.3599999999999990430 ) ) ;
#37205=ORIENTED_EDGE ( 'NONE', *, *, #9719, .F. ) ;
#37227=VECTOR ( 'NONE', #36907, 39.37007874015748143 ) ;
#37230=EDGE_LOOP ( 'NONE', ( #19884, #40567, #20895, #36480 ) ) ;
#37231=CARTESIAN_POINT ( 'NONE',  ( -0.1123123235486435112, -0.5135423695149557988, 0.1325268268875357536 ) ) ;
#37281=CARTESIAN_POINT ( 'NONE',  ( -0.1552051794442721455, 0.4812910476514246083, 0.09878871670238423275 ) ) ;
#37316=DIRECTION ( 'NONE',  ( -7.771561172376107616E-16, 7.170354002788761615E-17, -1.000000000000000000 ) ) ;
#37341=CARTESIAN_POINT ( 'NONE',  ( -0.1157263453858490138, -0.4799749855354071837, 0.1178658435936994486 ) ) ;
#37369=DIRECTION ( 'NONE',  ( -1.000000000000000000, -1.119941574063613413E-31, 7.771561172376109588E-16 ) ) ;
#37421=DIRECTION ( 'NONE',  ( -7.771561172376107616E-16, 7.170354002788761615E-17, -1.000000000000000000 ) ) ;
#37463=CARTESIAN_POINT ( 'NONE',  ( -0.1873388932668317575, 0.5325605939836577374, 0.3749999999999990008 ) ) ;
#37514=CARTESIAN_POINT ( 'NONE',  ( -0.1669433606228600819, 0.5138636982738132852, 0.1528658435937002569 ) ) ;
#37540=AXIS2_PLACEMENT_3D ( 'NONE', #26078, #38597, #33029 ) ;
#37579=PLANE ( 'NONE',  #21758 ) ;
#37580=ORIENTED_EDGE ( 'NONE', *, *, #27106, .F. ) ;
#37589=ORIENTED_EDGE ( 'NONE', *, *, #36823, .F. ) ;
#37615=AXIS2_PLACEMENT_3D ( 'NONE', #36947, #5680, #2598 ) ;
#37715=DIRECTION ( 'NONE',  ( 0.000000000000000000, 0.000000000000000000, -1.000000000000000000 ) ) ;
#37723=AXIS2_PLACEMENT_3D ( 'NONE', #38186, #25655, #4026 ) ;
#37731=AXIS2_PLACEMENT_3D ( 'NONE', #4359, #29050, #29464 ) ;
#37772=DIRECTION ( 'NONE',  ( -3.406373435249024214E-19, -1.000000000000000000, -7.170354002788761615E-17 ) ) ;
#37952=VERTEX_POINT ( 'NONE', #34981 ) ;
#37961=ADVANCED_FACE ( 'NONE', ( #10311 ), #10875, .T. ) ;
#38008=ORIENTED_EDGE ( 'NONE', *, *, #36565, .F. ) ;
#38042=VERTEX_POINT ( 'NONE', #39473 ) ;
#38052=ORIENTED_EDGE ( 'NONE', *, *, #20230, .F. ) ;
#38064=LINE ( 'NONE', #12775, #1580 ) ;
#38091=CARTESIAN_POINT ( 'NONE',  ( -0.1687956829044022500, 0.4914472887403520951, 0.1310621546645153179 ) ) ;
#38101=CARTESIAN_POINT ( 'NONE',  ( -0.1681560115201613526, 0.5223552577132001273, 0.1414989390318074358 ) ) ;
#38124=AXIS2_PLACEMENT_3D ( 'NONE', #20292, #16801, #19876 ) ;
#38130=ORIENTED_EDGE ( 'NONE', *, *, #20087, .T. ) ;
#38136=VECTOR ( 'NONE', #18369, 39.37007874015748143 ) ;
#38186=CARTESIAN_POINT ( 'NONE',  ( -0.1743922129835733248, -0.5166151207188712791, 0.09999999999999961697 ) ) ;
#38211=CARTESIAN_POINT ( 'NONE',  ( -1.019575837292303166, -0.04310840302197994911, 0.3599999999999993205 ) ) ;
#38236=CARTESIAN_POINT ( 'NONE',  ( -2.070754768975505034, -0.09959325338431362917, 0.3749999999999976130 ) ) ;
#38269=CYLINDRICAL_SURFACE ( 'NONE', #26494, 0.06000000000000021289 ) ;
#38274=CIRCLE ( 'NONE', #13325, 0.03000000000000022787 ) ;
#38309=DIRECTION ( 'NONE',  ( 7.771561172376107616E-16, -7.170354002788761615E-17, 1.000000000000000000 ) ) ;
#38341=ORIENTED_EDGE ( 'NONE', *, *, #24992, .T. ) ;
#38397=CIRCLE ( 'NONE', #32493, 2.001674066779347783 ) ;
#38465=AXIS2_PLACEMENT_3D ( 'NONE', #18030, #2207, #14747 ) ;
#38475=EDGE_CURVE ( 'NONE', #15629, #34573, #14841, .T. ) ;
#38543=VERTEX_POINT ( 'NONE', #29772 ) ;
#38560=CARTESIAN_POINT ( 'NONE',  ( -0.1157923916715166146, -0.5295015842444106280, 0.3181161673586325178 ) ) ;
#38597=DIRECTION ( 'NONE',  ( -7.771561172376107616E-16, 7.170354002788761615E-17, -1.000000000000000000 ) ) ;
#38601=CARTESIAN_POINT ( 'NONE',  ( -2.070754768975505034, -0.09959325338431362917, 0.09999999999999933942 ) ) ;
#38650=ORIENTED_EDGE ( 'NONE', *, *, #1372, .T. ) ;
#38670=CARTESIAN_POINT ( 'NONE',  ( -0.1623927644724122987, 0.5045516355107032558, 0.3253307341376669437 ) ) ;
#38671=CARTESIAN_POINT ( 'NONE',  ( -0.1129900121204593377, -0.5167580615068131378, 0.1415474730880576515 ) ) ;
#38776=EDGE_CURVE ( 'NONE', #40488, #12799, #1099, .T. ) ;
#38838=CARTESIAN_POINT ( 'NONE',  ( -0.1542132178619239902, 0.4779941576916497126, 0.1100664889103544625 ) ) ;
#38870=EDGE_CURVE ( 'NONE', #3414, #9996, #14864, .T. ) ;
#38919=( LENGTH_UNIT ( ) NAMED_UNIT ( * ) SI_UNIT ( $, .METRE. ) );
#39044=AXIS2_PLACEMENT_3D ( 'NONE', #33311, #20177, #7387 ) ;
#39054=CARTESIAN_POINT ( 'NONE',  ( -0.1583356623530577378, 0.4914777262839040151, 0.1012105261660898592 ) ) ;
#39082=CARTESIAN_POINT ( 'NONE',  ( -0.1710642718812837582, 0.4986889572247744651, 0.3032895567580805585 ) ) ;
#39139=EDGE_CURVE ( 'NONE', #34573, #8954, #6989, .T. ) ;
#39149=PRODUCT_DEFINITION_FORMATION_WITH_SPECIFIED_SOURCE ( 'ANY', '', #4853, .NOT_KNOWN. ) ;
#39154=CARTESIAN_POINT ( 'NONE',  ( -0.2666757540196700305, 0.4921670437878979398, 0.09999999999999879818 ) ) ;
#39161=EDGE_LOOP ( 'NONE', ( #605, #22907, #22440, #5560 ) ) ;
#39188=ADVANCED_FACE ( 'NONE', ( #25398 ), #19008, .F. ) ;
#39252=ORIENTED_EDGE ( 'NONE', *, *, #2946, .T. ) ;
#39259=CARTESIAN_POINT ( 'NONE',  ( -0.1621871387067581605, 0.5037941088976199966, 0.1094562450723028518 ) ) ;
#39260=VERTEX_POINT ( 'NONE', #12614 ) ;
#39296=EDGE_CURVE ( 'NONE', #34573, #12958, #32596, .T. ) ;
#39362=ORIENTED_EDGE ( 'NONE', *, *, #13917, .T. ) ;
#39371=ORIENTED_EDGE ( 'NONE', *, *, #15487, .F. ) ;
#39433=DIRECTION ( 'NONE',  ( 1.000000000000000000, 0.000000000000000000, 7.734859593387037307E-16 ) ) ;
#39437=CARTESIAN_POINT ( 'NONE',  ( -0.1061036098701634706, -0.4827967145417200179, 0.3599999999999998757 ) ) ;
#39454=EDGE_LOOP ( 'NONE', ( #5051, #19392, #35451, #12861, #10631, #22271 ) ) ;
#39473=CARTESIAN_POINT ( 'NONE',  ( -0.06908312040360713169, -0.09959325338431362917, 0.3602693341844379060 ) ) ;
#39485=DIRECTION ( 'NONE',  ( -0.4887635750372988364, -0.8724162812079787610, 3.838072908882819854E-15 ) ) ;
#39542=ORIENTED_EDGE ( 'NONE', *, *, #25336, .T. ) ;
#39600=DIRECTION ( 'NONE',  ( -0.05576617209162609834, -0.2535907321156583571, 0.9657027879401052228 ) ) ;
#39613=CARTESIAN_POINT ( 'NONE',  ( -0.1172150163383985644, -0.4875187859579053207, 0.1204312767266922934 ) ) ;
#39643=CARTESIAN_POINT ( 'NONE',  ( -2.070754768975505034, -0.09959325338431362917, 0.3749999999999976130 ) ) ;
#39656=VERTEX_POINT ( 'NONE', #16821 ) ;
#39717=DIRECTION ( 'NONE',  ( -0.1871397384865028934, -0.9823333030490228879, 6.429779641674037776E-17 ) ) ;
#39722=CARTESIAN_POINT ( 'NONE',  ( -0.2299999999999999267, 0.5182417262804744906, 0.3599999999999993205 ) ) ;
#39751=EDGE_LOOP ( 'NONE', ( #4135, #28647, #38052, #20156 ) ) ;
#39803=CARTESIAN_POINT ( 'NONE',  ( -0.1212602504878775439, -0.5073146173917496560, 0.3749999999999995559 ) ) ;
#39848=ADVANCED_FACE ( 'NONE', ( #20508 ), #28699, .T. ) ;
#39876=EDGE_CURVE ( 'NONE', #9065, #21878, #31723, .T. ) ;
#39891=DIRECTION ( 'NONE',  ( 1.000000000000000000, 1.118011712966791197E-31, -7.771561172376107616E-16 ) ) ;
#39908=CARTESIAN_POINT ( 'NONE',  ( -0.1103620673373381933, -0.5040504500049264314, 0.1035024533006822928 ) ) ;
#39999=ORIENTED_EDGE ( 'NONE', *, *, #40410, .T. ) ;
#40028=CYLINDRICAL_SURFACE ( 'NONE', #38465, 0.02999999999999998848 ) ;
#40038=ORIENTED_EDGE ( 'NONE', *, *, #38870, .T. ) ;
#40084=ADVANCED_FACE ( 'NONE', ( #29373 ), #12652, .T. ) ;
#40100=EDGE_CURVE ( 'NONE', #17948, #27939, #29106, .T. ) ;
#40103=SHAPE_REPRESENTATION ( 'Parallelogram front_FRONT', ( #27819 ), #33063 ) ;
#40119=DIRECTION ( 'NONE',  ( -7.771561172376107616E-16, 7.170354002788761615E-17, -1.000000000000000000 ) ) ;
#40175=DIRECTION ( 'NONE',  ( 0.3181970600707382246, -0.9480245940703960761, 3.970578237956065974E-16 ) ) ;
#40176=CIRCLE ( 'NONE', #15904, 0.06000000000000031697 ) ;
#40193=CARTESIAN_POINT ( 'NONE',  ( -0.2900000000000002576, 0.5182417262804744906, 0.09999999999999993616 ) ) ;
#40237=AXIS2_PLACEMENT_3D ( 'NONE', #1909, #26986, #30481 ) ;
#40259=CARTESIAN_POINT ( 'NONE',  ( -0.1638686671686047092, 0.5092269732922271031, 0.1413937977834339998 ) ) ;
#40307=CARTESIAN_POINT ( 'NONE',  ( -0.1150001097501270886, -0.4761628310996519065, 0.1178658437129749409 ) ) ;
#40336=CARTESIAN_POINT ( 'NONE',  ( -0.1112019842995528446, -0.5080904053907921991, 0.3498664773290688923 ) ) ;
#40385=ADVANCED_FACE ( 'NONE', ( #30586, #21944, #2409 ), #24415, .F. ) ;
#40410=EDGE_CURVE ( 'NONE', #4670, #28266, #7384, .T. ) ;
#40446=CARTESIAN_POINT ( 'NONE',  ( -0.2267371898560520682, -0.4872893062166330780, 0.3749999999999990008 ) ) ;
#40476=CARTESIAN_POINT ( 'NONE',  ( -0.1679467284717053865, 0.5217198260999535986, 0.1377606880063677042 ) ) ;
#40488=VERTEX_POINT ( 'NONE', #35081 ) ;
#40518=CARTESIAN_POINT ( 'NONE',  ( -0.1142670043590602175, -0.4723146173917087687, 0.1178658435937002397 ) ) ;
#40543=CARTESIAN_POINT ( 'NONE',  ( -0.1157923916715208196, -0.5295015842444287246, 0.3181161673586317962 ) ) ;
#40561=EDGE_LOOP ( 'NONE', ( #11816, #15936, #10559, #10509 ) ) ;
#40562=CARTESIAN_POINT ( 'NONE',  ( -0.1731185243557763487, 0.5373335498847187086, 0.3749999999999995559 ) ) ;
#40567=ORIENTED_EDGE ( 'NONE', *, *, #13486, .T. ) ;
#40581=CARTESIAN_POINT ( 'NONE',  ( -0.1999999999999997891, 0.5182417262804744906, 0.3749999999999995559 ) ) ;
#40586=EDGE_CURVE ( 'NONE', #15711, #31816, #10085, .T. ) ;
#40606=VERTEX_POINT ( 'NONE', #20269 ) ;
#40626=DIRECTION ( 'NONE',  ( 0.8724162812079758744, -0.4887635750373036103, 0.000000000000000000 ) ) ;
#40631=CARTESIAN_POINT ( 'NONE',  ( -0.1684323895664670556, 0.5231977504175358007, 0.3749999999999990008 ) ) ;
#40674=COLOUR_RGB('Light Blue',0.38,0.62,0.78);
#40675=FILL_AREA_STYLE_COLOUR('',#40674);
#40676=FILL_AREA_STYLE('',(#40675));
#40677=SURFACE_STYLE_FILL_AREA(#40676);
#40678=SURFACE_SIDE_STYLE('',(#40677));
#40679=SURFACE_STYLE_USAGE(.BOTH.,#40678);
#40680=PRESENTATION_STYLE_ASSIGNMENT((#40679));
#40714=STYLED_ITEM('',(#40680),#32046);
#40721=MECHANICAL_DESIGN_GEOMETRIC_PRESENTATION_REPRESENTATION('',(#40714),#11399);
ENDSEC;
END-ISO-10303-21;
